ISO-10303-21;
HEADER;
FILE_DESCRIPTION (('STEP AP214'),
    '1' );
FILE_NAME ('2-Bush.step',
    '2026-10-28T16:50:19',
    ( '' ),
    ( '' ),
    'SwSTEP 2.0',
    'SolidWorks 2024',
    '' );
FILE_SCHEMA (( 'AUTOMOTIVE_DESIGN' ));
ENDSEC;

DATA;
#4=ORIENTED_EDGE ( 'NONE', *, *, #2008, .F. ) ;
#7=ORIENTED_EDGE ( 'NONE', *, *, #437, .T. ) ;
#22=EDGE_CURVE ( 'NONE', #2924, #3020, #3177, .T. ) ;
#23=VERTEX_POINT ( 'NONE', #8844 ) ;
#28=DIRECTION ( 'NONE',  ( -1.000000000000000000, -0.000000000000000000, -0.000000000000000000 ) ) ;
#34=DIRECTION ( 'NONE',  ( 0.000000000000000000, 0.000000000000000000, 1.000000000000000000 ) ) ;
#42=ADVANCED_FACE ( 'NONE', ( #1448 ), #3565, .F. ) ;
#44=CARTESIAN_POINT ( 'NONE',  ( 0.000000000000000000, 0.000000000000000000, 0.000000000000000000 ) ) ;
#45=ORIENTED_EDGE ( 'NONE', *, *, #8118, .F. ) ;
#51=DIRECTION ( 'NONE',  ( 0.000000000000000000, 0.000000000000000000, 1.000000000000000000 ) ) ;
#59=AXIS2_PLACEMENT_3D ( 'NONE', #1262, #1856, #6375 ) ;
#66=ORIENTED_EDGE ( 'NONE', *, *, #5730, .F. ) ;
#69=LINE ( 'NONE', #4584, #4436 ) ;
#70=AXIS2_PLACEMENT_3D ( 'NONE', #3786, #2250, #5184 ) ;
#72=TOROIDAL_SURFACE ( 'NONE', #5447, 15.66147716702868209, 2.000000000000000000 ) ;
#73=ORIENTED_EDGE ( 'NONE', *, *, #437, .F. ) ;
#84=DIRECTION ( 'NONE',  ( -1.000000000000000000, -0.000000000000000000, -0.000000000000000000 ) ) ;
#85=VERTEX_POINT ( 'NONE', #733 ) ;
#92=UNCERTAINTY_MEASURE_WITH_UNIT (LENGTH_MEASURE( 1.000000000000000082E-05 ), #7663, 'distance_accuracy_value', 'NONE');
#93=CARTESIAN_POINT ( 'NONE',  ( 5.000000000000000000, 14.14213562373112154, -14.14213562373077870 ) ) ;
#100=AXIS2_PLACEMENT_3D ( 'NONE', #6905, #316, #3150 ) ;
#105=CARTESIAN_POINT ( 'NONE',  ( 4.000000000000000000, 20.00000000000120437, 1.559999999999680531 ) ) ;
#107=AXIS2_PLACEMENT_3D ( 'NONE', #3229, #1109, #5357 ) ;
#109=EDGE_LOOP ( 'NONE', ( #8068, #7356, #2708, #2295 ) ) ;
#113=CARTESIAN_POINT ( 'NONE',  ( 0.000000000000000000, 0.000000000000000000, 0.000000000000000000 ) ) ;
#115=CIRCLE ( 'NONE', #3792, 1.559999999998939346 ) ;
#126=AXIS2_PLACEMENT_3D ( 'NONE', #8460, #4038, #6303 ) ;
#133=DIRECTION ( 'NONE',  ( 1.000000000000000000, 0.000000000000000000, 0.000000000000000000 ) ) ;
#142=CARTESIAN_POINT ( 'NONE',  ( 2.000000000000000000, 0.000000000000000000, 0.000000000000000000 ) ) ;
#143=CIRCLE ( 'NONE', #3070, 1.559999999999098552 ) ;
#154=EDGE_CURVE ( 'NONE', #8069, #2437, #9010, .T. ) ;
#159=CARTESIAN_POINT ( 'NONE',  ( 0.000000000000000000, -18.47759065022712832, 6.903668647304566974 ) ) ;
#165=CARTESIAN_POINT ( 'NONE',  ( 3.499999999999999556, 0.000000000000000000, 0.000000000000000000 ) ) ;
#168=CARTESIAN_POINT ( 'NONE',  ( 0.000000000000000000, -14.14213562373112154, 15.70213562373564820 ) ) ;
#170=ORIENTED_EDGE ( 'NONE', *, *, #7706, .F. ) ;
#173=ORIENTED_EDGE ( 'NONE', *, *, #8062, .T. ) ;
#180=CARTESIAN_POINT ( 'NONE',  ( 4.000000000000000000, -14.14213562373248401, -14.14213562372942157 ) ) ;
#182=DIRECTION ( 'NONE',  ( 0.000000000000000000, 0.000000000000000000, 1.000000000000000000 ) ) ;
#189=AXIS2_PLACEMENT_3D ( 'NONE', #307, #3232, #6985 ) ;
#190=MANIFOLD_SOLID_BREP ( 'Radyus1', #2569 ) ;
#193=CYLINDRICAL_SURFACE ( 'NONE', #1753, 0.7499999999989250821 ) ;
#202=CARTESIAN_POINT ( 'NONE',  ( 0.000000000000000000, 2.755455298081544778E-15, -22.50000000000000000 ) ) ;
#204=DIRECTION ( 'NONE',  ( 0.000000000000000000, 0.000000000000000000, 1.000000000000000000 ) ) ;
#210=( NAMED_UNIT ( * ) PLANE_ANGLE_UNIT ( ) SI_UNIT ( $, .RADIAN. ) );
#238=ADVANCED_FACE ( 'NONE', ( #2419 ), #1693, .F. ) ;
#242=EDGE_LOOP ( 'NONE', ( #3695, #2216, #389, #7076 ) ) ;
#245=FACE_OUTER_BOUND ( 'NONE', #280, .T. ) ;
#246=CARTESIAN_POINT ( 'NONE',  ( 4.000000000000000000, -7.653668647303860872, -19.22759065022669134 ) ) ;
#255=ADVANCED_FACE ( 'NONE', ( #7915 ), #7696, .F. ) ;
#266=EDGE_LOOP ( 'NONE', ( #1164, #7378, #7869, #3274 ) ) ;
#268=DIRECTION ( 'NONE',  ( 0.000000000000000000, 0.000000000000000000, 1.000000000000000000 ) ) ;
#276=DIRECTION ( 'NONE',  ( -1.000000000000000000, -0.000000000000000000, -0.000000000000000000 ) ) ;
#278=DIRECTION ( 'NONE',  ( -1.000000000000000000, 0.000000000000000000, 0.000000000000000000 ) ) ;
#280=EDGE_LOOP ( 'NONE', ( #6235, #8043, #8671, #1683 ) ) ;
#281=ORIENTED_EDGE ( 'NONE', *, *, #5945, .F. ) ;
#282=PLANE ( 'NONE',  #9433 ) ;
#286=AXIS2_PLACEMENT_3D ( 'NONE', #6476, #7052, #8583 ) ;
#292=EDGE_LOOP ( 'NONE', ( #1795, #5038, #1091, #7202 ) ) ;
#294=PRODUCT_CONTEXT ( 'NONE', #1478, 'mechanical' ) ;
#298=CARTESIAN_POINT ( 'NONE',  ( 0.000000000000000000, 9.603694566548697359E-13, 20.00000000000290612 ) ) ;
#302=EDGE_LOOP ( 'NONE', ( #8368, #9024 ) ) ;
#307=CARTESIAN_POINT ( 'NONE',  ( 5.000000000000000000, 14.14213562373112154, -14.14213562373077870 ) ) ;
#309=ORIENTED_EDGE ( 'NONE', *, *, #4551, .T. ) ;
#311=ADVANCED_FACE ( 'NONE', ( #7870 ), #616, .F. ) ;
#312=ORIENTED_EDGE ( 'NONE', *, *, #829, .F. ) ;
#316=DIRECTION ( 'NONE',  ( -1.000000000000000000, 0.000000000000000000, 0.000000000000000000 ) ) ;
#322=LINE ( 'NONE', #3251, #1637 ) ;
#323=AXIS2_PLACEMENT_3D ( 'NONE', #1612, #9005, #2442 ) ;
#326=CARTESIAN_POINT ( 'NONE',  ( 4.000000000000000000, 9.605605015555367541E-13, 18.44000000000276884 ) ) ;
#328=EDGE_LOOP ( 'NONE', ( #7572, #3600, #1192, #3524 ) ) ;
#334=VERTEX_POINT ( 'NONE', #1065 ) ;
#336=CIRCLE ( 'NONE', #6014, 0.7499999999989250821 ) ;
#343=EDGE_CURVE ( 'NONE', #9037, #2987, #5640, .T. ) ;
#348=DIRECTION ( 'NONE',  ( 0.000000000000000000, 0.000000000000000000, -1.000000000000000000 ) ) ;
#357=AXIS2_PLACEMENT_3D ( 'NONE', #2834, #3402, #5045 ) ;
#361=CIRCLE ( 'NONE', #8500, 0.7500000000013684609 ) ;
#363=ORIENTED_EDGE ( 'NONE', *, *, #6358, .T. ) ;
#365=ORIENTED_EDGE ( 'NONE', *, *, #3412, .F. ) ;
#370=CARTESIAN_POINT ( 'NONE',  ( 0.000000000000000000, 18.47759065022658120, 7.653668647302884764 ) ) ;
#377=AXIS2_PLACEMENT_3D ( 'NONE', #180, #1518, #6041 ) ;
#384=DIRECTION ( 'NONE',  ( -1.000000000000000000, -0.000000000000000000, -0.000000000000000000 ) ) ;
#385=LINE ( 'NONE', #9079, #8335 ) ;
#389=ORIENTED_EDGE ( 'NONE', *, *, #8426, .T. ) ;
#390=CARTESIAN_POINT ( 'NONE',  ( 0.000000000000000000, 20.00000000000120437, 1.559999999999680531 ) ) ;
#391=FACE_OUTER_BOUND ( 'NONE', #7169, .T. ) ;
#422=VECTOR ( 'NONE', #8302, 1000.000000000000000 ) ;
#424=VERTEX_POINT ( 'NONE', #2296 ) ;
#427=EDGE_CURVE ( 'NONE', #424, #3685, #1571, .T. ) ;
#437=EDGE_CURVE ( 'NONE', #7541, #6226, #115, .T. ) ;
#439=AXIS2_PLACEMENT_3D ( 'NONE', #3196, #888, #5313 ) ;
#447=AXIS2_PLACEMENT_3D ( 'NONE', #6686, #8219, #4473 ) ;
#448=FACE_OUTER_BOUND ( 'NONE', #1573, .T. ) ;
#452=ORIENTED_EDGE ( 'NONE', *, *, #7402, .F. ) ;
#460=DIRECTION ( 'NONE',  ( 1.000000000000000000, 0.000000000000000000, 0.000000000000000000 ) ) ;
#475=ADVANCED_FACE ( 'NONE', ( #756 ), #4106, .T. ) ;
#478=DIRECTION ( 'NONE',  ( 0.7071067811865474617, 0.000000000000000000, -0.7071067811865474617 ) ) ;
#485=CIRCLE ( 'NONE', #2499, 17.50000000000000000 ) ;
#494=FACE_BOUND ( 'NONE', #302, .T. ) ;
#498=CARTESIAN_POINT ( 'NONE',  ( 5.000000000000000000, -18.47759065022712832, 6.903668647304566974 ) ) ;
#505=ORIENTED_EDGE ( 'NONE', *, *, #4882, .F. ) ;
#508=DIRECTION ( 'NONE',  ( -1.000000000000000000, -0.000000000000000000, -0.000000000000000000 ) ) ;
#509=DIRECTION ( 'NONE',  ( 0.000000000000000000, 0.000000000000000000, 1.000000000000000000 ) ) ;
#526=EDGE_LOOP ( 'NONE', ( #3501, #2271 ) ) ;
#528=VECTOR ( 'NONE', #5678, 1000.000000000000000 ) ;
#536=FACE_BOUND ( 'NONE', #7103, .T. ) ;
#542=FACE_BOUND ( 'NONE', #564, .T. ) ;
#546=AXIS2_PLACEMENT_3D ( 'NONE', #1226, #8727, #4975 ) ;
#554=DIRECTION ( 'NONE',  ( 1.000000000000000000, 0.000000000000000000, 0.000000000000000000 ) ) ;
#557=DIRECTION ( 'NONE',  ( -1.000000000000000000, -0.000000000000000000, -0.000000000000000000 ) ) ;
#560=CARTESIAN_POINT ( 'NONE',  ( 4.000000000000000000, 9.603694566548697359E-13, 20.00000000000290612 ) ) ;
#563=ORIENTED_EDGE ( 'NONE', *, *, #154, .F. ) ;
#564=EDGE_LOOP ( 'NONE', ( #4650, #3355 ) ) ;
#574=LINE ( 'NONE', #7151, #8849 ) ;
#575=AXIS2_PLACEMENT_3D ( 'NONE', #1520, #5762, #8108 ) ;
#586=FACE_BOUND ( 'NONE', #5148, .T. ) ;
#588=ORIENTED_EDGE ( 'NONE', *, *, #4774, .F. ) ;
#591=ORIENTED_EDGE ( 'NONE', *, *, #5521, .F. ) ;
#601=ORIENTED_EDGE ( 'NONE', *, *, #5718, .F. ) ;
#602=VERTEX_POINT ( 'NONE', #326 ) ;
#604=EDGE_LOOP ( 'NONE', ( #1437, #3375 ) ) ;
#607=CARTESIAN_POINT ( 'NONE',  ( 0.000000000000000000, 14.14213562373247868, 14.14213562373282329 ) ) ;
#609=CARTESIAN_POINT ( 'NONE',  ( 5.000000000000000000, 18.47759065022580316, -8.403668647301632433 ) ) ;
#616=CYLINDRICAL_SURFACE ( 'NONE', #3643, 0.7499999999989250821 ) ;
#618=EDGE_LOOP ( 'NONE', ( #4877, #690, #1083, #7069 ) ) ;
#627=AXIS2_PLACEMENT_3D ( 'NONE', #6856, #4109, #1035 ) ;
#634=DIRECTION ( 'NONE',  ( 1.000000000000000000, 0.000000000000000000, 0.000000000000000000 ) ) ;
#658=CARTESIAN_POINT ( 'NONE',  ( 4.000000000000000000, -18.47759065022712832, 7.653668647304757044 ) ) ;
#665=CARTESIAN_POINT ( 'NONE',  ( 19.00000000000000000, 1.673048428422632513E-15, -13.66147716702868031 ) ) ;
#669=AXIS2_PLACEMENT_3D ( 'NONE', #44, #3585, #3155 ) ;
#679=AXIS2_PLACEMENT_3D ( 'NONE', #8913, #3105, #4816 ) ;
#680=CARTESIAN_POINT ( 'NONE',  ( 5.000000000000000000, 7.653668647302530381, 18.47759065022802716 ) ) ;
#682=CARTESIAN_POINT ( 'NONE',  ( 4.000000000000000888, 0.000000000000000000, 0.000000000000000000 ) ) ;
#683=ORIENTED_EDGE ( 'NONE', *, *, #6737, .T. ) ;
#690=ORIENTED_EDGE ( 'NONE', *, *, #4956, .T. ) ;
#692=ORIENTED_EDGE ( 'NONE', *, *, #1393, .T. ) ;
#694=VERTEX_POINT ( 'NONE', #1906 ) ;
#697=CARTESIAN_POINT ( 'NONE',  ( 4.000000000000000000, 7.653668647300657213, -18.47759065022568237 ) ) ;
#700=EDGE_CURVE ( 'NONE', #4346, #4647, #8117, .T. ) ;
#708=CARTESIAN_POINT ( 'NONE',  ( 4.000000000000000000, -7.653668647301985040, 17.72759065022987812 ) ) ;
#711=EDGE_CURVE ( 'NONE', #2638, #8944, #9177, .T. ) ;
#725=DIRECTION ( 'NONE',  ( -1.000000000000000000, -0.000000000000000000, -0.000000000000000000 ) ) ;
#729=LINE ( 'NONE', #3662, #9036 ) ;
#732=ORIENTED_EDGE ( 'NONE', *, *, #4518, .F. ) ;
#733=CARTESIAN_POINT ( 'NONE',  ( 0.000000000000000000, 0.000000000000000000, 15.66147716702868209 ) ) ;
#736=CYLINDRICAL_SURFACE ( 'NONE', #4488, 22.50000000000000000 ) ;
#745=DIRECTION ( 'NONE',  ( 1.000000000000000000, 0.000000000000000000, 0.000000000000000000 ) ) ;
#747=LINE ( 'NONE', #3680, #3464 ) ;
#750=CARTESIAN_POINT ( 'NONE',  ( 0.000000000000000000, -18.47759065022712832, 8.403668647304948891 ) ) ;
#756=FACE_OUTER_BOUND ( 'NONE', #328, .T. ) ;
#778=DIRECTION ( 'NONE',  ( 0.000000000000000000, 0.000000000000000000, -1.000000000000000000 ) ) ;
#779=DIRECTION ( 'NONE',  ( 0.000000000000000000, 0.000000000000000000, 1.000000000000000000 ) ) ;
#782=AXIS2_PLACEMENT_3D ( 'NONE', #7082, #5747, #1994 ) ;
#786=CARTESIAN_POINT ( 'NONE',  ( 4.000000000000000000, -9.628187502531647418E-13, -19.99999999999950262 ) ) ;
#787=CARTESIAN_POINT ( 'NONE',  ( 0.000000000000000000, 14.14213562373112154, -14.14213562373077870 ) ) ;
#792=CARTESIAN_POINT ( 'NONE',  ( 5.000000000000000000, -18.47759065022790637, -7.653668647299759265 ) ) ;
#803=FACE_OUTER_BOUND ( 'NONE', #3328, .T. ) ;
#807=CIRCLE ( 'NONE', #357, 22.00000000000000711 ) ;
#811=CARTESIAN_POINT ( 'NONE',  ( 0.000000000000000000, -20.00000000000120437, -1.559999999999665432 ) ) ;
#812=VECTOR ( 'NONE', #8914, 1000.000000000000000 ) ;
#813=CARTESIAN_POINT ( 'NONE',  ( 4.000000000000000000, -20.00000000000120437, -1.559999999999665432 ) ) ;
#814=EDGE_CURVE ( 'NONE', #1024, #7251, #8573, .T. ) ;
#823=EDGE_CURVE ( 'NONE', #8944, #2638, #9332, .T. ) ;
#825=AXIS2_PLACEMENT_3D ( 'NONE', #1228, #9202, #9397 ) ;
#827=EDGE_LOOP ( 'NONE', ( #4902, #309, #5550, #5021 ) ) ;
#829=EDGE_CURVE ( 'NONE', #6912, #2947, #5199, .T. ) ;
#839=FACE_OUTER_BOUND ( 'NONE', #4855, .T. ) ;
#840=DIRECTION ( 'NONE',  ( 0.000000000000000000, 0.000000000000000000, 1.000000000000000000 ) ) ;
#847=EDGE_CURVE ( 'NONE', #2113, #8405, #2894, .T. ) ;
#852=CARTESIAN_POINT ( 'NONE',  ( 4.000000000000000000, -7.653668647301985040, 19.22759065022772873 ) ) ;
#855=AXIS2_PLACEMENT_3D ( 'NONE', #607, #9439, #1415 ) ;
#863=DIRECTION ( 'NONE',  ( 0.000000000000000000, 0.000000000000000000, -1.000000000000000000 ) ) ;
#869=AXIS2_PLACEMENT_3D ( 'NONE', #2272, #7890, #5920 ) ;
#874=DIRECTION ( 'NONE',  ( -1.000000000000000000, 0.000000000000000000, 0.000000000000000000 ) ) ;
#875=CYLINDRICAL_SURFACE ( 'NONE', #2570, 0.7499999999982936982 ) ;
#887=AXIS2_PLACEMENT_3D ( 'NONE', #3361, #3310, #9168 ) ;
#888=DIRECTION ( 'NONE',  ( -1.000000000000000000, 0.000000000000000000, 0.000000000000000000 ) ) ;
#889=EDGE_CURVE ( 'NONE', #3554, #2688, #4126, .T. ) ;
#904=ORIENTED_EDGE ( 'NONE', *, *, #5117, .F. ) ;
#905=LINE ( 'NONE', #3836, #422 ) ;
#908=DIRECTION ( 'NONE',  ( 0.000000000000000000, 0.000000000000000000, 1.000000000000000000 ) ) ;
#925=DIRECTION ( 'NONE',  ( 0.000000000000000000, 0.000000000000000000, 1.000000000000000000 ) ) ;
#928=CARTESIAN_POINT ( 'NONE',  ( 0.000000000000000000, 14.14213562373247868, 15.70213562373191962 ) ) ;
#929=AXIS2_PLACEMENT_3D ( 'NONE', #1666, #4598, #1516 ) ;
#930=ORIENTED_EDGE ( 'NONE', *, *, #2550, .T. ) ;
#943=VERTEX_POINT ( 'NONE', #8191 ) ;
#965=FACE_OUTER_BOUND ( 'NONE', #8996, .T. ) ;
#969=ORIENTED_EDGE ( 'NONE', *, *, #1072, .F. ) ;
#978=ORIENTED_EDGE ( 'NONE', *, *, #1905, .F. ) ;
#993=DIRECTION ( 'NONE',  ( -1.000000000000000000, 0.000000000000000000, 0.000000000000000000 ) ) ;
#995=ORIENTED_EDGE ( 'NONE', *, *, #2557, .F. ) ;
#996=APPLICATION_CONTEXT ( 'automotive_design' ) ;
#1000=VERTEX_POINT ( 'NONE', #4592 ) ;
#1008=EDGE_CURVE ( 'NONE', #5740, #5476, #5509, .T. ) ;
#1023=EDGE_CURVE ( 'NONE', #8436, #8187, #4586, .T. ) ;
#1024=VERTEX_POINT ( 'NONE', #3238 ) ;
#1035=DIRECTION ( 'NONE',  ( 0.000000000000000000, 0.000000000000000000, 1.000000000000000000 ) ) ;
#1037=AXIS2_PLACEMENT_3D ( 'NONE', #792, #84, #5222 ) ;
#1041=VERTEX_POINT ( 'NONE', #6086 ) ;
#1054=ORIENTED_EDGE ( 'NONE', *, *, #4209, .T. ) ;
#1065=CARTESIAN_POINT ( 'NONE',  ( 0.000000000000000000, -9.626277053524975217E-13, -21.56000000000076966 ) ) ;
#1068=CARTESIAN_POINT ( 'NONE',  ( 4.000000000000000000, 20.00000000000120437, 7.412591687719288072E-13 ) ) ;
#1072=EDGE_CURVE ( 'NONE', #6494, #1522, #8028, .T. ) ;
#1079=AXIS2_PLACEMENT_3D ( 'NONE', #1419, #8677, #509 ) ;
#1083=ORIENTED_EDGE ( 'NONE', *, *, #2430, .T. ) ;
#1091=ORIENTED_EDGE ( 'NONE', *, *, #1126, .T. ) ;
#1093=CIRCLE ( 'NONE', #5560, 13.66147716702868031 ) ;
#1102=CYLINDRICAL_SURFACE ( 'NONE', #1185, 0.7500000000000015543 ) ;
#1109=DIRECTION ( 'NONE',  ( 1.000000000000000000, 0.000000000000000000, 0.000000000000000000 ) ) ;
#1113=FACE_OUTER_BOUND ( 'NONE', #6047, .T. ) ;
#1114=ORIENTED_EDGE ( 'NONE', *, *, #4456, .T. ) ;
#1115=VERTEX_POINT ( 'NONE', #1542 ) ;
#1117=ORIENTED_EDGE ( 'NONE', *, *, #2214, .T. ) ;
#1118=CARTESIAN_POINT ( 'NONE',  ( 2.000000000000000000, 1.917977788252103204E-15, -15.66147716702868209 ) ) ;
#1124=CARTESIAN_POINT ( 'NONE',  ( 0.000000000000000000, 14.14213562373247868, 12.58213562373372341 ) ) ;
#1126=EDGE_CURVE ( 'NONE', #1041, #1656, #729, .T. ) ;
#1128=LINE ( 'NONE', #9193, #1741 ) ;
#1129=ORIENTED_EDGE ( 'NONE', *, *, #6545, .T. ) ;
#1140=ADVANCED_FACE ( 'NONE', ( #7398 ), #5247, .F. ) ;
#1141=CARTESIAN_POINT ( 'NONE',  ( 4.000000000000000000, -14.14213562373112154, 15.70213562373564820 ) ) ;
#1145=ORIENTED_EDGE ( 'NONE', *, *, #7525, .T. ) ;
#1149=CARTESIAN_POINT ( 'NONE',  ( 0.000000000000000000, 0.000000000000000000, -22.00000000000000711 ) ) ;
#1150=DIRECTION ( 'NONE',  ( 0.000000000000000000, 0.000000000000000000, 1.000000000000000000 ) ) ;
#1164=ORIENTED_EDGE ( 'NONE', *, *, #8986, .F. ) ;
#1165=FACE_BOUND ( 'NONE', #7878, .T. ) ;
#1173=ORIENTED_EDGE ( 'NONE', *, *, #4774, .T. ) ;
#1178=EDGE_CURVE ( 'NONE', #8069, #1024, #6744, .T. ) ;
#1182=ORIENTED_EDGE ( 'NONE', *, *, #427, .T. ) ;
#1185=AXIS2_PLACEMENT_3D ( 'NONE', #4041, #384, #7548 ) ;
#1192=ORIENTED_EDGE ( 'NONE', *, *, #6007, .F. ) ;
#1200=EDGE_LOOP ( 'NONE', ( #3293, #365 ) ) ;
#1201=AXIS2_PLACEMENT_3D ( 'NONE', #5797, #2183, #34 ) ;
#1202=EDGE_LOOP ( 'NONE', ( #1388, #7892 ) ) ;
#1204=DIRECTION ( 'NONE',  ( 0.000000000000000000, 0.000000000000000000, 1.000000000000000000 ) ) ;
#1206=DIRECTION ( 'NONE',  ( 0.000000000000000000, 0.000000000000000000, 1.000000000000000000 ) ) ;
#1207=DIRECTION ( 'NONE',  ( 0.000000000000000000, 0.000000000000000000, 1.000000000000000000 ) ) ;
#1216=EDGE_CURVE ( 'NONE', #5087, #1485, #7499, .T. ) ;
#1223=ORIENTED_EDGE ( 'NONE', *, *, #2885, .F. ) ;
#1226=CARTESIAN_POINT ( 'NONE',  ( 4.000000000000000000, 0.000000000000000000, 0.000000000000000000 ) ) ;
#1227=FACE_OUTER_BOUND ( 'NONE', #292, .T. ) ;
#1228=CARTESIAN_POINT ( 'NONE',  ( 4.000000000000000000, 7.653668647302530381, 18.47759065022802716 ) ) ;
#1244=ORIENTED_EDGE ( 'NONE', *, *, #5697, .F. ) ;
#1249=CARTESIAN_POINT ( 'NONE',  ( 4.000000000000000000, -18.47759065022790637, -6.903668647298391470 ) ) ;
#1252=FACE_BOUND ( 'NONE', #5996, .T. ) ;
#1261=DIRECTION ( 'NONE',  ( -1.000000000000000000, -0.000000000000000000, -0.000000000000000000 ) ) ;
#1262=CARTESIAN_POINT ( 'NONE',  ( 5.000000000000000000, -14.14213562373248401, -14.14213562372942157 ) ) ;
#1265=LINE ( 'NONE', #5751, #7011 ) ;
#1289=EDGE_LOOP ( 'NONE', ( #3491, #8589 ) ) ;
#1290=ADVANCED_FACE ( 'NONE', ( #3944 ), #5350, .F. ) ;
#1291=CARTESIAN_POINT ( 'NONE',  ( 5.000000000000000000, 9.605605015555367541E-13, 18.44000000000276884 ) ) ;
#1305=FACE_BOUND ( 'NONE', #6622, .T. ) ;
#1308=ADVANCED_FACE ( 'NONE', ( #4620 ), #1102, .F. ) ;
#1309=DIRECTION ( 'NONE',  ( 0.000000000000000000, 0.000000000000000000, 1.000000000000000000 ) ) ;
#1310=DIRECTION ( 'NONE',  ( -1.000000000000000000, -0.000000000000000000, -0.000000000000000000 ) ) ;
#1314=ADVANCED_FACE ( 'NONE', ( #965 ), #9034, .F. ) ;
#1328=ORIENTED_EDGE ( 'NONE', *, *, #9361, .T. ) ;
#1333=AXIS2_PLACEMENT_3D ( 'NONE', #7194, #7239, #1380 ) ;
#1342=ORIENTED_EDGE ( 'NONE', *, *, #3024, .T. ) ;
#1354=AXIS2_PLACEMENT_3D ( 'NONE', #2476, #5401, #6176 ) ;
#1357=DIRECTION ( 'NONE',  ( 0.000000000000000000, 0.000000000000000000, 1.000000000000000000 ) ) ;
#1362=EDGE_CURVE ( 'NONE', #334, #9368, #7161, .T. ) ;
#1378=ORIENTED_EDGE ( 'NONE', *, *, #5924, .F. ) ;
#1380=DIRECTION ( 'NONE',  ( 0.000000000000000000, 0.000000000000000000, 1.000000000000000000 ) ) ;
#1383=AXIS2_PLACEMENT_3D ( 'NONE', #8049, #8244, #2231 ) ;
#1385=DIRECTION ( 'NONE',  ( 0.000000000000000000, 0.000000000000000000, 1.000000000000000000 ) ) ;
#1388=ORIENTED_EDGE ( 'NONE', *, *, #3626, .F. ) ;
#1393=EDGE_CURVE ( 'NONE', #5764, #2437, #574, .T. ) ;
#1394=DIRECTION ( 'NONE',  ( 0.000000000000000000, 0.000000000000000000, 1.000000000000000000 ) ) ;
#1396=CYLINDRICAL_SURFACE ( 'NONE', #9154, 0.7499999999982936982 ) ;
#1406=AXIS2_PLACEMENT_3D ( 'NONE', #298, #9077, #3313 ) ;
#1415=DIRECTION ( 'NONE',  ( 0.000000000000000000, 0.000000000000000000, 1.000000000000000000 ) ) ;
#1419=CARTESIAN_POINT ( 'NONE',  ( 5.000000000000000000, -20.00000000000120437, 2.661998082081668380E-12 ) ) ;
#1422=DIRECTION ( 'NONE',  ( -1.000000000000000000, -0.000000000000000000, -0.000000000000000000 ) ) ;
#1428=EDGE_CURVE ( 'NONE', #3148, #7251, #5582, .T. ) ;
#1437=ORIENTED_EDGE ( 'NONE', *, *, #7525, .F. ) ;
#1446=FACE_BOUND ( 'NONE', #7222, .T. ) ;
#1448=FACE_OUTER_BOUND ( 'NONE', #5684, .T. ) ;
#1456=EDGE_LOOP ( 'NONE', ( #2022, #930 ) ) ;
#1460=ORIENTED_EDGE ( 'NONE', *, *, #8353, .T. ) ;
#1478=APPLICATION_CONTEXT ( 'automotive_design' ) ;
#1485=VERTEX_POINT ( 'NONE', #2880 ) ;
#1496=CARTESIAN_POINT ( 'NONE',  ( 0.000000000000000000, 9.605605015555367541E-13, 18.44000000000276884 ) ) ;
#1497=EDGE_LOOP ( 'NONE', ( #8449, #7236 ) ) ;
#1502=CARTESIAN_POINT ( 'NONE',  ( 0.000000000000000000, -7.653668647303860872, -17.72759065022311731 ) ) ;
#1511=CARTESIAN_POINT ( 'NONE',  ( 0.000000000000000000, -14.14213562373112154, 14.14213562373418220 ) ) ;
#1516=DIRECTION ( 'NONE',  ( 0.000000000000000000, 0.000000000000000000, 1.000000000000000000 ) ) ;
#1518=DIRECTION ( 'NONE',  ( 1.000000000000000000, 0.000000000000000000, 0.000000000000000000 ) ) ;
#1520=CARTESIAN_POINT ( 'NONE',  ( 4.000000000000000000, 20.00000000000120437, 7.412591687719288072E-13 ) ) ;
#1522=VERTEX_POINT ( 'NONE', #5233 ) ;
#1525=EDGE_CURVE ( 'NONE', #1041, #6239, #3642, .T. ) ;
#1529=DIRECTION ( 'NONE',  ( 0.000000000000000000, 0.000000000000000000, -1.000000000000000000 ) ) ;
#1530=ORIENTED_EDGE ( 'NONE', *, *, #8852, .F. ) ;
#1539=ADVANCED_FACE ( 'NONE', ( #803 ), #1578, .F. ) ;
#1542=CARTESIAN_POINT ( 'NONE',  ( 0.000000000000000000, 14.14213562373112154, -12.58213562373077821 ) ) ;
#1547=ORIENTED_EDGE ( 'NONE', *, *, #3751, .T. ) ;
#1556=AXIS2_PLACEMENT_3D ( 'NONE', #8802, #7509, #2223 ) ;
#1559=ORIENTED_EDGE ( 'NONE', *, *, #7403, .F. ) ;
#1562=DIRECTION ( 'NONE',  ( 0.000000000000000000, 0.000000000000000000, -1.000000000000000000 ) ) ;
#1567=CARTESIAN_POINT ( 'NONE',  ( 5.000000000000000000, -14.14213562373248401, -15.70213562373165850 ) ) ;
#1568=CARTESIAN_POINT ( 'NONE',  ( 0.000000000000000000, -9.628187502531647418E-13, -19.99999999999950262 ) ) ;
#1569=ORIENTED_EDGE ( 'NONE', *, *, #3257, .T. ) ;
#1571=LINE ( 'NONE', #3781, #2876 ) ;
#1573=EDGE_LOOP ( 'NONE', ( #1976, #6178, #6644, #2482 ) ) ;
#1578=CYLINDRICAL_SURFACE ( 'NONE', #2575, 1.560000000000000719 ) ;
#1593=ADVANCED_FACE ( 'NONE', ( #8689 ), #2108, .F. ) ;
#1594=( LENGTH_UNIT ( ) NAMED_UNIT ( * ) SI_UNIT ( .MILLI., .METRE. ) );
#1598=DIRECTION ( 'NONE',  ( 0.000000000000000000, 0.000000000000000000, 1.000000000000000000 ) ) ;
#1612=CARTESIAN_POINT ( 'NONE',  ( 0.000000000000000000, 7.653668647302530381, 18.47759065022802716 ) ) ;
#1614=AXIS2_PLACEMENT_3D ( 'NONE', #6760, #5504, #4539 ) ;
#1625=SHAPE_REPRESENTATION ( '2-Bush', ( #1614 ), #7287 ) ;
#1637=VECTOR ( 'NONE', #8391, 1000.000000000000000 ) ;
#1638=CARTESIAN_POINT ( 'NONE',  ( 0.000000000000000000, 7.653668647300657213, -18.47759065022568237 ) ) ;
#1648=AXIS2_PLACEMENT_3D ( 'NONE', #5972, #3802, #6600 ) ;
#1650=CARTESIAN_POINT ( 'NONE',  ( 4.000000000000000000, -7.653668647303860872, -18.47759065022490432 ) ) ;
#1652=AXIS2_PLACEMENT_3D ( 'NONE', #165, #4477, #2373 ) ;
#1653=DIRECTION ( 'NONE',  ( 0.000000000000000000, 0.000000000000000000, 1.000000000000000000 ) ) ;
#1656=VERTEX_POINT ( 'NONE', #8264 ) ;
#1666=CARTESIAN_POINT ( 'NONE',  ( 0.000000000000000000, 0.000000000000000000, 0.000000000000000000 ) ) ;
#1670=ORIENTED_EDGE ( 'NONE', *, *, #7859, .T. ) ;
#1679=DIRECTION ( 'NONE',  ( 0.000000000000000000, 0.000000000000000000, 1.000000000000000000 ) ) ;
#1681=DIRECTION ( 'NONE',  ( -1.000000000000000000, -0.000000000000000000, -0.000000000000000000 ) ) ;
#1683=ORIENTED_EDGE ( 'NONE', *, *, #5010, .T. ) ;
#1693=CYLINDRICAL_SURFACE ( 'NONE', #9301, 0.7500000000017874591 ) ;
#1710=CARTESIAN_POINT ( 'NONE',  ( 0.000000000000000000, 0.000000000000000000, -22.00000000000000711 ) ) ;
#1712=EDGE_LOOP ( 'NONE', ( #3856, #4 ) ) ;
#1724=FACE_OUTER_BOUND ( 'NONE', #2138, .T. ) ;
#1729=AXIS2_PLACEMENT_3D ( 'NONE', #1837, #874, #1204 ) ;
#1735=EDGE_CURVE ( 'NONE', #4149, #9366, #8587, .T. ) ;
#1737=ORIENTED_EDGE ( 'NONE', *, *, #2850, .T. ) ;
#1741=VECTOR ( 'NONE', #2630, 1000.000000000000000 ) ;
#1748=ORIENTED_EDGE ( 'NONE', *, *, #4956, .F. ) ;
#1753=AXIS2_PLACEMENT_3D ( 'NONE', #2402, #1681, #908 ) ;
#1755=CONICAL_SURFACE ( 'NONE', #3437, 22.50000000000000000, 0.7853981633974447263 ) ;
#1762=DIRECTION ( 'NONE',  ( 0.000000000000000000, 0.000000000000000000, -1.000000000000000000 ) ) ;
#1767=DIRECTION ( 'NONE',  ( 1.000000000000000000, 0.000000000000000000, 0.000000000000000000 ) ) ;
#1775=ADVANCED_FACE ( 'NONE', ( #7867 ), #2596, .F. ) ;
#1795=ORIENTED_EDGE ( 'NONE', *, *, #8757, .F. ) ;
#1804=CIRCLE ( 'NONE', #9164, 0.7500000000012114754 ) ;
#1822=CIRCLE ( 'NONE', #3356, 1.560000000001466436 ) ;
#1825=AXIS2_PLACEMENT_3D ( 'NONE', #7134, #554, #4071 ) ;
#1833=EDGE_CURVE ( 'NONE', #3385, #8070, #6412, .T. ) ;
#1835=VERTEX_POINT ( 'NONE', #6524 ) ;
#1837=CARTESIAN_POINT ( 'NONE',  ( 0.000000000000000000, -14.14213562373112154, 14.14213562373418220 ) ) ;
#1840=CARTESIAN_POINT ( 'NONE',  ( 0.000000000000000000, 14.14213562373112154, -14.14213562373077870 ) ) ;
#1845=EDGE_LOOP ( 'NONE', ( #6698, #6887, #2168, #9187 ) ) ;
#1847=ORIENTED_EDGE ( 'NONE', *, *, #5753, .F. ) ;
#1850=EDGE_CURVE ( 'NONE', #9368, #334, #8406, .T. ) ;
#1853=EDGE_CURVE ( 'NONE', #7405, #5068, #9308, .T. ) ;
#1856=DIRECTION ( 'NONE',  ( -1.000000000000000000, -0.000000000000000000, -0.000000000000000000 ) ) ;
#1858=ORIENTED_EDGE ( 'NONE', *, *, #814, .F. ) ;
#1860=CIRCLE ( 'NONE', #2634, 0.7499999999989250821 ) ;
#1861=EDGE_LOOP ( 'NONE', ( #1342, #1182, #2045, #1530 ) ) ;
#1870=AXIS2_PLACEMENT_3D ( 'NONE', #6510, #2134, #5835 ) ;
#1872=CARTESIAN_POINT ( 'NONE',  ( 0.000000000000000000, -18.47759065022712832, 7.653668647304757044 ) ) ;
#1873=AXIS2_PLACEMENT_3D ( 'NONE', #5970, #7353, #2317 ) ;
#1884=AXIS2_PLACEMENT_3D ( 'NONE', #7079, #4868, #7803 ) ;
#1887=ADVANCED_FACE ( 'NONE', ( #2147 ), #4497, .F. ) ;
#1891=ORIENTED_EDGE ( 'NONE', *, *, #889, .T. ) ;
#1894=FACE_BOUND ( 'NONE', #6267, .T. ) ;
#1895=VECTOR ( 'NONE', #8504, 1000.000000000000000 ) ;
#1897=CARTESIAN_POINT ( 'NONE',  ( 0.000000000000000000, -18.47759065022790637, -6.903668647298391470 ) ) ;
#1900=VERTEX_POINT ( 'NONE', #5078 ) ;
#1905=EDGE_CURVE ( 'NONE', #9340, #1115, #2236, .T. ) ;
#1906=CARTESIAN_POINT ( 'NONE',  ( 4.000000000000000000, -14.14213562373248401, -12.58213562372718641 ) ) ;
#1910=DIRECTION ( 'NONE',  ( -1.000000000000000000, -0.000000000000000000, -0.000000000000000000 ) ) ;
#1912=EDGE_CURVE ( 'NONE', #1900, #9366, #1804, .T. ) ;
#1916=EDGE_LOOP ( 'NONE', ( #6537, #5907, #4701, #9273 ) ) ;
#1917=AXIS2_PLACEMENT_3D ( 'NONE', #2531, #4875, #6144 ) ;
#1941=FACE_OUTER_BOUND ( 'NONE', #9328, .T. ) ;
#1944=AXIS2_PLACEMENT_3D ( 'NONE', #7080, #6324, #8523 ) ;
#1954=ADVANCED_FACE ( 'NONE', ( #4313 ), #6621, .F. ) ;
#1959=DIRECTION ( 'NONE',  ( -1.000000000000000000, -0.000000000000000000, -0.000000000000000000 ) ) ;
#1962=DIRECTION ( 'NONE',  ( -1.000000000000000000, -0.000000000000000000, -0.000000000000000000 ) ) ;
#1963=AXIS2_PLACEMENT_3D ( 'NONE', #2467, #9307, #1973 ) ;
#1964=MECHANICAL_DESIGN_GEOMETRIC_PRESENTATION_REPRESENTATION('',(#2424),#7788);
#1971=CIRCLE ( 'NONE', #5964, 2.000000000000000000 ) ;
#1973=DIRECTION ( 'NONE',  ( 0.000000000000000000, 0.000000000000000000, 1.000000000000000000 ) ) ;
#1976=ORIENTED_EDGE ( 'NONE', *, *, #3015, .T. ) ;
#1977=AXIS2_PLACEMENT_3D ( 'NONE', #786, #5841, #2952 ) ;
#1985=CARTESIAN_POINT ( 'NONE',  ( 0.000000000000000000, 0.000000000000000000, 0.000000000000000000 ) ) ;
#1986=VERTEX_POINT ( 'NONE', #4550 ) ;
#1990=FACE_BOUND ( 'NONE', #9454, .T. ) ;
#1994=DIRECTION ( 'NONE',  ( 0.000000000000000000, 0.000000000000000000, -1.000000000000000000 ) ) ;
#1996=ORIENTED_EDGE ( 'NONE', *, *, #1912, .T. ) ;
#1999=ORIENTED_EDGE ( 'NONE', *, *, #8529, .T. ) ;
#2004=EDGE_CURVE ( 'NONE', #8070, #6226, #5464, .T. ) ;
#2007=CARTESIAN_POINT ( 'NONE',  ( 5.000000000000000000, -14.14213562373112154, 14.14213562373418220 ) ) ;
#2008=EDGE_CURVE ( 'NONE', #7855, #4159, #361, .T. ) ;
#2010=ORIENTED_EDGE ( 'NONE', *, *, #829, .T. ) ;
#2022=ORIENTED_EDGE ( 'NONE', *, *, #5730, .T. ) ;
#2030=FACE_BOUND ( 'NONE', #5175, .T. ) ;
#2031=ORIENTED_EDGE ( 'NONE', *, *, #5155, .F. ) ;
#2035=FACE_BOUND ( 'NONE', #4302, .T. ) ;
#2038=FACE_OUTER_BOUND ( 'NONE', #1916, .T. ) ;
#2045=ORIENTED_EDGE ( 'NONE', *, *, #6465, .T. ) ;
#2054=CARTESIAN_POINT ( 'NONE',  ( 4.000000000000000000, -7.653668647303860872, -17.72759065022311731 ) ) ;
#2055=DIRECTION ( 'NONE',  ( -1.000000000000000000, -0.000000000000000000, -0.000000000000000000 ) ) ;
#2056=VERTEX_POINT ( 'NONE', #3978 ) ;
#2064=ORIENTED_EDGE ( 'NONE', *, *, #5718, .T. ) ;
#2070=AXIS2_PLACEMENT_3D ( 'NONE', #1638, #8979, #204 ) ;
#2094=CARTESIAN_POINT ( 'NONE',  ( 4.000000000000000888, 2.143131898507868248E-15, -17.50000000000000000 ) ) ;
#2100=DIRECTION ( 'NONE',  ( 1.000000000000000000, 0.000000000000000000, 0.000000000000000000 ) ) ;
#2108=CYLINDRICAL_SURFACE ( 'NONE', #5022, 0.7500000000012114754 ) ;
#2113=VERTEX_POINT ( 'NONE', #9337 ) ;
#2114=CIRCLE ( 'NONE', #6277, 0.7500000000001915135 ) ;
#2120=DIRECTION ( 'NONE',  ( -1.000000000000000000, -0.000000000000000000, -0.000000000000000000 ) ) ;
#2131=DIRECTION ( 'NONE',  ( 0.000000000000000000, 0.000000000000000000, 1.000000000000000000 ) ) ;
#2134=DIRECTION ( 'NONE',  ( -1.000000000000000000, -0.000000000000000000, -0.000000000000000000 ) ) ;
#2138=EDGE_LOOP ( 'NONE', ( #8490, #1891, #2158, #2010 ) ) ;
#2147=FACE_OUTER_BOUND ( 'NONE', #4203, .T. ) ;
#2150=DIRECTION ( 'NONE',  ( -1.000000000000000000, -0.000000000000000000, -0.000000000000000000 ) ) ;
#2158=ORIENTED_EDGE ( 'NONE', *, *, #9316, .T. ) ;
#2161=ADVANCED_FACE ( 'NONE', ( #4021 ), #4876, .F. ) ;
#2167=FACE_BOUND ( 'NONE', #1497, .T. ) ;
#2168=ORIENTED_EDGE ( 'NONE', *, *, #5155, .T. ) ;
#2183=DIRECTION ( 'NONE',  ( -1.000000000000000000, 0.000000000000000000, 0.000000000000000000 ) ) ;
#2211=CARTESIAN_POINT ( 'NONE',  ( 4.000000000000000000, 14.14213562373247868, 14.14213562373282329 ) ) ;
#2212=DIRECTION ( 'NONE',  ( -1.000000000000000000, -0.000000000000000000, -0.000000000000000000 ) ) ;
#2214=EDGE_CURVE ( 'NONE', #2638, #9368, #1128, .T. ) ;
#2216=ORIENTED_EDGE ( 'NONE', *, *, #3051, .F. ) ;
#2218=CIRCLE ( 'NONE', #2070, 0.7500000000012114754 ) ;
#2221=FACE_OUTER_BOUND ( 'NONE', #9411, .T. ) ;
#2222=CARTESIAN_POINT ( 'NONE',  ( 3.499999999999999556, 0.000000000000000000, 0.000000000000000000 ) ) ;
#2223=DIRECTION ( 'NONE',  ( 0.000000000000000000, 0.000000000000000000, 1.000000000000000000 ) ) ;
#2230=CARTESIAN_POINT ( 'NONE',  ( 0.000000000000000000, 18.47759065022658120, 7.653668647302884764 ) ) ;
#2231=DIRECTION ( 'NONE',  ( 0.000000000000000000, 0.000000000000000000, 1.000000000000000000 ) ) ;
#2236=LINE ( 'NONE', #8054, #5497 ) ;
#2245=EDGE_LOOP ( 'NONE', ( #8109, #4946, #9230, #505 ) ) ;
#2248=CIRCLE ( 'NONE', #7622, 0.7500000000017874591 ) ;
#2250=DIRECTION ( 'NONE',  ( -1.000000000000000000, -0.000000000000000000, -0.000000000000000000 ) ) ;
#2264=AXIS2_PLACEMENT_3D ( 'NONE', #7211, #4379, #6361 ) ;
#2271=ORIENTED_EDGE ( 'NONE', *, *, #3994, .F. ) ;
#2272=CARTESIAN_POINT ( 'NONE',  ( 5.000000000000000000, 18.47759065022580316, -7.653668647301631545 ) ) ;
#2284=CARTESIAN_POINT ( 'NONE',  ( 4.000000000000000000, -7.653668647301985040, 18.47759065022880520 ) ) ;
#2295=ORIENTED_EDGE ( 'NONE', *, *, #3626, .T. ) ;
#2296=CARTESIAN_POINT ( 'NONE',  ( 4.000000000000000000, 18.47759065022658120, 6.903668647304224137 ) ) ;
#2317=DIRECTION ( 'NONE',  ( 0.000000000000000000, 0.000000000000000000, -1.000000000000000000 ) ) ;
#2325=EDGE_LOOP ( 'NONE', ( #6236, #692, #563, #2031 ) ) ;
#2327=CARTESIAN_POINT ( 'NONE',  ( 5.000000000000000000, 7.653668647302530381, 18.47759065022802716 ) ) ;
#2329=DIRECTION ( 'NONE',  ( 1.000000000000000000, 0.000000000000000000, 0.000000000000000000 ) ) ;
#2351=ORIENTED_EDGE ( 'NONE', *, *, #2550, .F. ) ;
#2373=DIRECTION ( 'NONE',  ( 0.000000000000000000, 0.000000000000000000, -1.000000000000000000 ) ) ;
#2378=VECTOR ( 'NONE', #276, 1000.000000000000000 ) ;
#2379=CARTESIAN_POINT ( 'NONE',  ( 0.000000000000000000, -20.00000000000120437, 2.661998082081668380E-12 ) ) ;
#2384=SHAPE_REPRESENTATION_RELATIONSHIP ( 'NONE' , 'NONE' ,  #1625, #4626 ) ;
#2388=CARTESIAN_POINT ( 'NONE',  ( 4.000000000000000000, 7.653668647300657213, -18.47759065022568237 ) ) ;
#2402=CARTESIAN_POINT ( 'NONE',  ( 5.000000000000000000, -7.653668647301985040, 18.47759065022880520 ) ) ;
#2419=FACE_OUTER_BOUND ( 'NONE', #2245, .T. ) ;
#2420=EDGE_LOOP ( 'NONE', ( #4901, #9272 ) ) ;
#2422=DIRECTION ( 'NONE',  ( 0.000000000000000000, 0.000000000000000000, 1.000000000000000000 ) ) ;
#2424=STYLED_ITEM('',(#9515),#190);
#2429=CIRCLE ( 'NONE', #7026, 0.7500000000001915135 ) ;
#2430=EDGE_CURVE ( 'NONE', #2916, #8405, #385, .T. ) ;
#2437=VERTEX_POINT ( 'NONE', #4088 ) ;
#2442=DIRECTION ( 'NONE',  ( 0.000000000000000000, 0.000000000000000000, 1.000000000000000000 ) ) ;
#2465=DIRECTION ( 'NONE',  ( 0.7071067811865474617, 8.659560562354932858E-17, 0.7071067811865474617 ) ) ;
#2467=CARTESIAN_POINT ( 'NONE',  ( 5.000000000000000000, -7.653668647303860872, -18.47759065022490432 ) ) ;
#2476=CARTESIAN_POINT ( 'NONE',  ( 5.000000000000000000, 20.00000000000120437, 7.412591687719288072E-13 ) ) ;
#2482=ORIENTED_EDGE ( 'NONE', *, *, #6531, .F. ) ;
#2484=CARTESIAN_POINT ( 'NONE',  ( 0.000000000000000000, 14.14213562373247868, 14.14213562373282329 ) ) ;
#2490=CARTESIAN_POINT ( 'NONE',  ( 0.000000000000000000, -18.47759065022790637, -7.653668647299759265 ) ) ;
#2491=ORIENTED_EDGE ( 'NONE', *, *, #8177, .T. ) ;
#2499=AXIS2_PLACEMENT_3D ( 'NONE', #6357, #2120, #1207 ) ;
#2504=EDGE_LOOP ( 'NONE', ( #173, #3409, #7269, #6350 ) ) ;
#2505=AXIS2_PLACEMENT_3D ( 'NONE', #6684, #8086, #778 ) ;
#2515=DIRECTION ( 'NONE',  ( 1.000000000000000000, 0.000000000000000000, 0.000000000000000000 ) ) ;
#2517=CARTESIAN_POINT ( 'NONE',  ( 0.000000000000000000, 7.653668647302530381, 17.72759065022973246 ) ) ;
#2521=ORIENTED_EDGE ( 'NONE', *, *, #1023, .T. ) ;
#2524=ORIENTED_EDGE ( 'NONE', *, *, #7908, .T. ) ;
#2531=CARTESIAN_POINT ( 'NONE',  ( 0.000000000000000000, -14.14213562373248401, -14.14213562372942157 ) ) ;
#2536=FACE_BOUND ( 'NONE', #9197, .T. ) ;
#2542=CARTESIAN_POINT ( 'NONE',  ( 5.000000000000000000, -9.626277053524975217E-13, -21.56000000000076966 ) ) ;
#2550=EDGE_CURVE ( 'NONE', #5750, #3148, #807, .T. ) ;
#2557=EDGE_CURVE ( 'NONE', #8610, #4346, #6447, .T. ) ;
#2564=AXIS2_PLACEMENT_3D ( 'NONE', #5991, #6039, #8194 ) ;
#2569=CLOSED_SHELL ( 'NONE', ( #475, #9166, #5459, #8347, #8526, #4360, #1775, #2703, #6052, #1140, #5949, #1308, #1593, #238, #4738, #3143, #311, #3299, #8357, #7241, #8471, #4044, #1954, #9270, #3261, #7014, #8345, #3241, #4710, #8473, #2720, #1290, #1887, #1314, #7688, #42, #1539, #5048, #2161, #3947, #4916, #8528, #255, #6151, #4509, #7208, #5630 ) ) ;
#2570=AXIS2_PLACEMENT_3D ( 'NONE', #2327, #3810, #3276 ) ;
#2575=AXIS2_PLACEMENT_3D ( 'NONE', #93, #6535, #51 ) ;
#2577=DIRECTION ( 'NONE',  ( 0.000000000000000000, 0.000000000000000000, -1.000000000000000000 ) ) ;
#2578=VECTOR ( 'NONE', #7350, 1000.000000000000000 ) ;
#2585=ORIENTED_EDGE ( 'NONE', *, *, #9139, .F. ) ;
#2596=CYLINDRICAL_SURFACE ( 'NONE', #4572, 1.560000000001466436 ) ;
#2607=CARTESIAN_POINT ( 'NONE',  ( 5.000000000000000000, 14.14213562373112154, -15.70213562373078098 ) ) ;
#2609=ORIENTED_EDGE ( 'NONE', *, *, #1362, .F. ) ;
#2622=VERTEX_POINT ( 'NONE', #8782 ) ;
#2623=DIRECTION ( 'NONE',  ( 1.000000000000000000, 0.000000000000000000, 0.000000000000000000 ) ) ;
#2630=DIRECTION ( 'NONE',  ( -1.000000000000000000, -0.000000000000000000, -0.000000000000000000 ) ) ;
#2632=ORIENTED_EDGE ( 'NONE', *, *, #700, .F. ) ;
#2634=AXIS2_PLACEMENT_3D ( 'NONE', #4062, #6906, #6143 ) ;
#2636=CARTESIAN_POINT ( 'NONE',  ( 0.000000000000000000, 7.653668647302530381, 18.47759065022802716 ) ) ;
#2638=VERTEX_POINT ( 'NONE', #6676 ) ;
#2644=ORIENTED_EDGE ( 'NONE', *, *, #5753, .T. ) ;
#2656=EDGE_LOOP ( 'NONE', ( #7957, #9298 ) ) ;
#2666=ORIENTED_EDGE ( 'NONE', *, *, #1428, .F. ) ;
#2672=DIRECTION ( 'NONE',  ( -1.000000000000000000, -0.000000000000000000, -0.000000000000000000 ) ) ;
#2679=ORIENTED_EDGE ( 'NONE', *, *, #2214, .F. ) ;
#2688=VERTEX_POINT ( 'NONE', #852 ) ;
#2695=PRODUCT_DEFINITION_FORMATION_WITH_SPECIFIED_SOURCE ( 'ANY', '', #6699, .NOT_KNOWN. ) ;
#2703=ADVANCED_FACE ( 'NONE', ( #3691 ), #6628, .F. ) ;
#2707=PLANE ( 'NONE',  #2264 ) ;
#2708=ORIENTED_EDGE ( 'NONE', *, *, #6531, .T. ) ;
#2709=CIRCLE ( 'NONE', #855, 1.559999999999096776 ) ;
#2711=EDGE_LOOP ( 'NONE', ( #4423, #8156 ) ) ;
#2720=ADVANCED_FACE ( 'NONE', ( #1724 ), #193, .F. ) ;
#2725=DIRECTION ( 'NONE',  ( 0.000000000000000000, 0.000000000000000000, -1.000000000000000000 ) ) ;
#2739=EDGE_CURVE ( 'NONE', #6084, #4903, #8401, .T. ) ;
#2746=LINE ( 'NONE', #3401, #528 ) ;
#2754=AXIS2_PLACEMENT_3D ( 'NONE', #8950, #2329, #5259 ) ;
#2756=DIRECTION ( 'NONE',  ( -1.000000000000000000, -0.000000000000000000, -0.000000000000000000 ) ) ;
#2760=DIRECTION ( 'NONE',  ( 0.000000000000000000, 0.000000000000000000, -1.000000000000000000 ) ) ;
#2777=LINE ( 'NONE', #5665, #3930 ) ;
#2781=CARTESIAN_POINT ( 'NONE',  ( 5.000000000000000000, 7.653668647300657213, -17.72759065022447089 ) ) ;
#2790=CIRCLE ( 'NONE', #1870, 17.50000000000000000 ) ;
#2798=DIRECTION ( 'NONE',  ( 0.000000000000000000, 0.000000000000000000, 1.000000000000000000 ) ) ;
#2806=FACE_OUTER_BOUND ( 'NONE', #266, .T. ) ;
#2828=CARTESIAN_POINT ( 'NONE',  ( 5.000000000000000000, -7.653668647301985040, 18.47759065022880520 ) ) ;
#2831=VECTOR ( 'NONE', #6778, 1000.000000000000000 ) ;
#2834=CARTESIAN_POINT ( 'NONE',  ( 0.000000000000000000, 0.000000000000000000, 0.000000000000000000 ) ) ;
#2837=DIRECTION ( 'NONE',  ( -0.7071067811865500152, 8.659560562354903276E-17, -0.7071067811865451302 ) ) ;
#2850=EDGE_CURVE ( 'NONE', #8610, #5692, #8656, .T. ) ;
#2855=DIRECTION ( 'NONE',  ( 0.000000000000000000, 0.000000000000000000, 1.000000000000000000 ) ) ;
#2858=AXIS2_PLACEMENT_3D ( 'NONE', #7587, #1910, #6828 ) ;
#2862=EDGE_LOOP ( 'NONE', ( #5189, #7200, #4391, #3191 ) ) ;
#2872=ORIENTED_EDGE ( 'NONE', *, *, #343, .T. ) ;
#2876=VECTOR ( 'NONE', #2150, 1000.000000000000000 ) ;
#2880=CARTESIAN_POINT ( 'NONE',  ( 0.000000000000000000, 14.14213562373112154, -15.70213562373078098 ) ) ;
#2885=EDGE_CURVE ( 'NONE', #4565, #602, #5593, .T. ) ;
#2890=DIRECTION ( 'NONE',  ( -1.000000000000000000, -0.000000000000000000, -0.000000000000000000 ) ) ;
#2894=CIRCLE ( 'NONE', #6436, 1.560000000001466436 ) ;
#2896=VECTOR ( 'NONE', #2890, 1000.000000000000000 ) ;
#2899=FACE_OUTER_BOUND ( 'NONE', #7412, .T. ) ;
#2916=VERTEX_POINT ( 'NONE', #1141 ) ;
#2917=DIRECTION ( 'NONE',  ( -1.000000000000000000, 0.000000000000000000, 0.000000000000000000 ) ) ;
#2924=VERTEX_POINT ( 'NONE', #4169 ) ;
#2938=CARTESIAN_POINT ( 'NONE',  ( 0.000000000000000000, 0.000000000000000000, 0.000000000000000000 ) ) ;
#2940=CARTESIAN_POINT ( 'NONE',  ( 2.000000000000000000, 0.000000000000000000, 15.66147716702868209 ) ) ;
#2947=VERTEX_POINT ( 'NONE', #6386 ) ;
#2952=DIRECTION ( 'NONE',  ( 0.000000000000000000, 0.000000000000000000, -1.000000000000000000 ) ) ;
#2954=DIRECTION ( 'NONE',  ( -1.000000000000000000, 0.000000000000000000, 0.000000000000000000 ) ) ;
#2960=DIRECTION ( 'NONE',  ( 0.000000000000000000, 0.000000000000000000, -1.000000000000000000 ) ) ;
#2966=CARTESIAN_POINT ( 'NONE',  ( 5.000000000000000000, 9.603694566548697359E-13, 21.56000000000303984 ) ) ;
#2972=EDGE_LOOP ( 'NONE', ( #7131, #2609 ) ) ;
#2979=DIRECTION ( 'NONE',  ( 1.000000000000000000, 0.000000000000000000, 0.000000000000000000 ) ) ;
#2981=DIRECTION ( 'NONE',  ( -1.000000000000000000, -0.000000000000000000, -0.000000000000000000 ) ) ;
#2982=AXIS2_PLACEMENT_3D ( 'NONE', #658, #5171, #8730 ) ;
#2986=AXIS2_PLACEMENT_3D ( 'NONE', #3311, #8216, #6206 ) ;
#2987=VERTEX_POINT ( 'NONE', #2054 ) ;
#2992=ORIENTED_EDGE ( 'NONE', *, *, #5521, .T. ) ;
#3015=EDGE_CURVE ( 'NONE', #7382, #2622, #3907, .T. ) ;
#3020=VERTEX_POINT ( 'NONE', #2094 ) ;
#3024=EDGE_CURVE ( 'NONE', #4140, #424, #7743, .T. ) ;
#3033=CARTESIAN_POINT ( 'NONE',  ( 5.000000000000000000, 14.14213562373247868, 12.58213562373372341 ) ) ;
#3050=ORIENTED_EDGE ( 'NONE', *, *, #7174, .T. ) ;
#3051=EDGE_CURVE ( 'NONE', #85, #3983, #7586, .T. ) ;
#3062=CARTESIAN_POINT ( 'NONE',  ( 0.000000000000000000, 0.000000000000000000, 0.000000000000000000 ) ) ;
#3066=DIRECTION ( 'NONE',  ( 0.000000000000000000, 0.000000000000000000, 1.000000000000000000 ) ) ;
#3070=AXIS2_PLACEMENT_3D ( 'NONE', #2211, #2979, #863 ) ;
#3081=DIRECTION ( 'NONE',  ( 0.000000000000000000, 0.000000000000000000, 1.000000000000000000 ) ) ;
#3094=ORIENTED_EDGE ( 'NONE', *, *, #8986, .T. ) ;
#3096=( NAMED_UNIT ( * ) SI_UNIT ( $, .STERADIAN. ) SOLID_ANGLE_UNIT ( ) );
#3105=DIRECTION ( 'NONE',  ( -1.000000000000000000, -0.000000000000000000, -0.000000000000000000 ) ) ;
#3135=ORIENTED_EDGE ( 'NONE', *, *, #1853, .T. ) ;
#3138=DIRECTION ( 'NONE',  ( -1.000000000000000000, -0.000000000000000000, -0.000000000000000000 ) ) ;
#3140=EDGE_CURVE ( 'NONE', #7436, #8998, #8153, .T. ) ;
#3143=ADVANCED_FACE ( 'NONE', ( #448 ), #7797, .F. ) ;
#3148=VERTEX_POINT ( 'NONE', #1710 ) ;
#3150=DIRECTION ( 'NONE',  ( 0.000000000000000000, 0.000000000000000000, 1.000000000000000000 ) ) ;
#3155=DIRECTION ( 'NONE',  ( 0.000000000000000000, 0.000000000000000000, 1.000000000000000000 ) ) ;
#3166=VECTOR ( 'NONE', #508, 1000.000000000000000 ) ;
#3177=CIRCLE ( 'NONE', #9002, 17.50000000000000000 ) ;
#3191=ORIENTED_EDGE ( 'NONE', *, *, #8118, .T. ) ;
#3195=ORIENTED_EDGE ( 'NONE', *, *, #1853, .F. ) ;
#3196=CARTESIAN_POINT ( 'NONE',  ( 0.000000000000000000, -7.653668647303860872, -18.47759065022490432 ) ) ;
#3207=AXIS2_PLACEMENT_3D ( 'NONE', #2284, #5214, #1562 ) ;
#3210=AXIS2_PLACEMENT_3D ( 'NONE', #4529, #4482, #6753 ) ;
#3229=CARTESIAN_POINT ( 'NONE',  ( 0.000000000000000000, 0.000000000000000000, 0.000000000000000000 ) ) ;
#3232=DIRECTION ( 'NONE',  ( -1.000000000000000000, -0.000000000000000000, -0.000000000000000000 ) ) ;
#3238=CARTESIAN_POINT ( 'NONE',  ( 0.4999999999999935052, 0.000000000000000000, 22.50000000000000000 ) ) ;
#3241=ADVANCED_FACE ( 'NONE', ( #536, #3513, #1446, #7844, #5825, #4189, #7115, #5738, #7305, #3418, #4336, #2167, #2030, #5690, #9374, #1252, #5642, #586 ), #2707, .T. ) ;
#3247=CIRCLE ( 'NONE', #1556, 22.00000000000000711 ) ;
#3251=CARTESIAN_POINT ( 'NONE',  ( 5.000000000000000000, -7.653668647301985040, 19.22759065022772873 ) ) ;
#3257=EDGE_CURVE ( 'NONE', #6494, #5769, #3788, .T. ) ;
#3261=ADVANCED_FACE ( 'NONE', ( #6407 ), #4957, .T. ) ;
#3267=LINE ( 'NONE', #9032, #6221 ) ;
#3270=DIRECTION ( 'NONE',  ( -1.000000000000000000, -0.000000000000000000, -0.000000000000000000 ) ) ;
#3274=ORIENTED_EDGE ( 'NONE', *, *, #814, .T. ) ;
#3276=DIRECTION ( 'NONE',  ( 0.000000000000000000, 0.000000000000000000, 1.000000000000000000 ) ) ;
#3281=EDGE_CURVE ( 'NONE', #5764, #1835, #5947, .T. ) ;
#3282=ORIENTED_EDGE ( 'NONE', *, *, #3051, .T. ) ;
#3286=DIRECTION ( 'NONE',  ( 1.000000000000000000, 0.000000000000000000, 0.000000000000000000 ) ) ;
#3287=AXIS2_PLACEMENT_3D ( 'NONE', #560, #7139, #4125 ) ;
#3293=ORIENTED_EDGE ( 'NONE', *, *, #5348, .F. ) ;
#3299=ADVANCED_FACE ( 'NONE', ( #7984 ), #1396, .F. ) ;
#3310=DIRECTION ( 'NONE',  ( -1.000000000000000000, 0.000000000000000000, 0.000000000000000000 ) ) ;
#3311=CARTESIAN_POINT ( 'NONE',  ( 5.000000000000000000, -9.628187502531647418E-13, -19.99999999999950262 ) ) ;
#3313=DIRECTION ( 'NONE',  ( 0.000000000000000000, 0.000000000000000000, 1.000000000000000000 ) ) ;
#3316=ORIENTED_EDGE ( 'NONE', *, *, #3994, .T. ) ;
#3324=DIRECTION ( 'NONE',  ( -1.000000000000000000, -0.000000000000000000, -0.000000000000000000 ) ) ;
#3328=EDGE_LOOP ( 'NONE', ( #3720, #2491, #6748, #683 ) ) ;
#3331=AXIS2_PLACEMENT_3D ( 'NONE', #7876, #4221, #8551 ) ;
#3334=CARTESIAN_POINT ( 'NONE',  ( 4.000000000000000000, 14.14213562373112154, -14.14213562373077870 ) ) ;
#3338=CARTESIAN_POINT ( 'NONE',  ( 4.000000000000000000, 7.653668647300657213, -17.72759065022447089 ) ) ;
#3348=LINE ( 'NONE', #3579, #4733 ) ;
#3355=ORIENTED_EDGE ( 'NONE', *, *, #823, .F. ) ;
#3356=AXIS2_PLACEMENT_3D ( 'NONE', #5143, #5969, #8130 ) ;
#3361=CARTESIAN_POINT ( 'NONE',  ( 0.000000000000000000, 9.603694566548697359E-13, 20.00000000000290612 ) ) ;
#3367=VERTEX_POINT ( 'NONE', #1496 ) ;
#3369=CARTESIAN_POINT ( 'NONE',  ( 4.000000000000000000, -14.14213562373248401, -15.70213562373165850 ) ) ;
#3375=ORIENTED_EDGE ( 'NONE', *, *, #3751, .F. ) ;
#3385=VERTEX_POINT ( 'NONE', #105 ) ;
#3388=ORIENTED_EDGE ( 'NONE', *, *, #711, .T. ) ;
#3391=ORIENTED_EDGE ( 'NONE', *, *, #2004, .T. ) ;
#3401=CARTESIAN_POINT ( 'NONE',  ( 0.000000000000000000, 2.143131898507868248E-15, -17.50000000000000000 ) ) ;
#3402=DIRECTION ( 'NONE',  ( -1.000000000000000000, -0.000000000000000000, -0.000000000000000000 ) ) ;
#3409=ORIENTED_EDGE ( 'NONE', *, *, #6002, .T. ) ;
#3411=CARTESIAN_POINT ( 'NONE',  ( 4.000000000000000000, -18.47759065022790637, -7.653668647299759265 ) ) ;
#3412=EDGE_CURVE ( 'NONE', #7436, #694, #7632, .T. ) ;
#3417=CARTESIAN_POINT ( 'NONE',  ( 5.000000000000000000, -14.14213562373248401, -14.14213562372942157 ) ) ;
#3418=FACE_BOUND ( 'NONE', #2711, .T. ) ;
#3427=CYLINDRICAL_SURFACE ( 'NONE', #7537, 1.560000000000134168 ) ;
#3437=AXIS2_PLACEMENT_3D ( 'NONE', #4453, #7375, #840 ) ;
#3451=VERTEX_POINT ( 'NONE', #665 ) ;
#3461=DIRECTION ( 'NONE',  ( -1.000000000000000000, 0.000000000000000000, 0.000000000000000000 ) ) ;
#3462=CARTESIAN_POINT ( 'NONE',  ( 4.000000000000000000, 18.47759065022580316, -7.653668647301631545 ) ) ;
#3464=VECTOR ( 'NONE', #3823, 1000.000000000000000 ) ;
#3468=FACE_BOUND ( 'NONE', #5407, .T. ) ;
#3472=DIRECTION ( 'NONE',  ( 0.000000000000000000, 0.000000000000000000, 1.000000000000000000 ) ) ;
#3491=ORIENTED_EDGE ( 'NONE', *, *, #3024, .F. ) ;
#3495=AXIS2_PLACEMENT_3D ( 'NONE', #4394, #745, #6615 ) ;
#3496=CARTESIAN_POINT ( 'NONE',  ( 0.000000000000000000, 18.47759065022580316, -7.653668647301631545 ) ) ;
#3501=ORIENTED_EDGE ( 'NONE', *, *, #5261, .F. ) ;
#3509=LINE ( 'NONE', #5733, #3793 ) ;
#3512=DIRECTION ( 'NONE',  ( -1.000000000000000000, -0.000000000000000000, -0.000000000000000000 ) ) ;
#3513=FACE_OUTER_BOUND ( 'NONE', #1456, .T. ) ;
#3524=ORIENTED_EDGE ( 'NONE', *, *, #8426, .F. ) ;
#3525=ORIENTED_EDGE ( 'NONE', *, *, #1216, .T. ) ;
#3529=DIRECTION ( 'NONE',  ( 0.000000000000000000, 0.000000000000000000, 1.000000000000000000 ) ) ;
#3554=VERTEX_POINT ( 'NONE', #708 ) ;
#3558=CIRCLE ( 'NONE', #1406, 1.560000000000134168 ) ;
#3565=CYLINDRICAL_SURFACE ( 'NONE', #869, 0.7500000000000015543 ) ;
#3570=CARTESIAN_POINT ( 'NONE',  ( 0.000000000000000000, 7.653668647302530381, 19.22759065022631830 ) ) ;
#3579=CARTESIAN_POINT ( 'NONE',  ( 5.000000000000000000, -18.47759065022712832, 8.403668647304948891 ) ) ;
#3581=LINE ( 'NONE', #609, #7835 ) ;
#3585=DIRECTION ( 'NONE',  ( -1.000000000000000000, -0.000000000000000000, -0.000000000000000000 ) ) ;
#3599=EDGE_CURVE ( 'NONE', #5692, #4647, #905, .T. ) ;
#3600=ORIENTED_EDGE ( 'NONE', *, *, #6843, .T. ) ;
#3611=DIRECTION ( 'NONE',  ( -1.000000000000000000, -0.000000000000000000, -0.000000000000000000 ) ) ;
#3614=ORIENTED_EDGE ( 'NONE', *, *, #22, .F. ) ;
#3619=CARTESIAN_POINT ( 'NONE',  ( 2.000000000000000000, 0.000000000000000000, 0.000000000000000000 ) ) ;
#3626=EDGE_CURVE ( 'NONE', #5267, #6180, #2429, .T. ) ;
#3628=DIRECTION ( 'NONE',  ( -1.000000000000000000, 0.000000000000000000, 0.000000000000000000 ) ) ;
#3632=CYLINDRICAL_SURFACE ( 'NONE', #1079, 1.560000000002327303 ) ;
#3637=CIRCLE ( 'NONE', #107, 15.66147716702868209 ) ;
#3642=CIRCLE ( 'NONE', #9156, 1.560000000002327303 ) ;
#3643=AXIS2_PLACEMENT_3D ( 'NONE', #2828, #9355, #5040 ) ;
#3647=AXIS2_PLACEMENT_3D ( 'NONE', #8344, #1767, #7006 ) ;
#3659=CARTESIAN_POINT ( 'NONE',  ( 4.000000000000000000, -9.626277053524975217E-13, -21.56000000000076966 ) ) ;
#3662=CARTESIAN_POINT ( 'NONE',  ( 5.000000000000000000, -20.00000000000120437, 1.560000000004989174 ) ) ;
#3666=CIRCLE ( 'NONE', #3210, 1.559999999999098552 ) ;
#3673=DIRECTION ( 'NONE',  ( 0.000000000000000000, 0.000000000000000000, 1.000000000000000000 ) ) ;
#3680=CARTESIAN_POINT ( 'NONE',  ( 5.000000000000000000, -7.653668647301985040, 17.72759065022987812 ) ) ;
#3684=DIRECTION ( 'NONE',  ( -1.000000000000000000, -0.000000000000000000, -0.000000000000000000 ) ) ;
#3685=VERTEX_POINT ( 'NONE', #6104 ) ;
#3687=CARTESIAN_POINT ( 'NONE',  ( 0.000000000000000000, 20.00000000000120437, 7.412591687719288072E-13 ) ) ;
#3691=FACE_OUTER_BOUND ( 'NONE', #4591, .T. ) ;
#3695=ORIENTED_EDGE ( 'NONE', *, *, #6843, .F. ) ;
#3703=PRODUCT_DEFINITION_SHAPE ( 'NONE', 'NONE',  #9048 ) ;
#3709=EDGE_CURVE ( 'NONE', #8944, #334, #3988, .T. ) ;
#3716=DIRECTION ( 'NONE',  ( 0.000000000000000000, -1.000000000000000000, 0.000000000000000000 ) ) ;
#3720=ORIENTED_EDGE ( 'NONE', *, *, #1216, .F. ) ;
#3722=CIRCLE ( 'NONE', #1729, 1.560000000001466436 ) ;
#3733=DIRECTION ( 'NONE',  ( -1.000000000000000000, 0.000000000000000000, 0.000000000000000000 ) ) ;
#3749=AXIS2_PLACEMENT_3D ( 'NONE', #5653, #1261, #4966 ) ;
#3751=EDGE_CURVE ( 'NONE', #943, #4838, #4110, .T. ) ;
#3773=CYLINDRICAL_SURFACE ( 'NONE', #929, 13.66147716702868031 ) ;
#3780=CIRCLE ( 'NONE', #2564, 1.560000000001466436 ) ;
#3781=CARTESIAN_POINT ( 'NONE',  ( 5.000000000000000000, 18.47759065022658120, 6.903668647304224137 ) ) ;
#3786=CARTESIAN_POINT ( 'NONE',  ( 5.000000000000000000, -20.00000000000120437, 2.661998082081668380E-12 ) ) ;
#3788=CIRCLE ( 'NONE', #6561, 0.7500000000000006661 ) ;
#3789=ORIENTED_EDGE ( 'NONE', *, *, #9316, .F. ) ;
#3790=ORIENTED_EDGE ( 'NONE', *, *, #9361, .F. ) ;
#3792=AXIS2_PLACEMENT_3D ( 'NONE', #3687, #2917, #4556 ) ;
#3793=VECTOR ( 'NONE', #2756, 1000.000000000000000 ) ;
#3800=DIRECTION ( 'NONE',  ( -1.000000000000000000, -0.000000000000000000, -0.000000000000000000 ) ) ;
#3802=DIRECTION ( 'NONE',  ( 1.000000000000000000, 0.000000000000000000, 0.000000000000000000 ) ) ;
#3810=DIRECTION ( 'NONE',  ( -1.000000000000000000, -0.000000000000000000, -0.000000000000000000 ) ) ;
#3817=ORIENTED_EDGE ( 'NONE', *, *, #8614, .T. ) ;
#3823=DIRECTION ( 'NONE',  ( -1.000000000000000000, -0.000000000000000000, -0.000000000000000000 ) ) ;
#3836=CARTESIAN_POINT ( 'NONE',  ( 5.000000000000000000, 7.653668647302530381, 17.72759065022973246 ) ) ;
#3856=ORIENTED_EDGE ( 'NONE', *, *, #8353, .F. ) ;
#3862=VECTOR ( 'NONE', #28, 1000.000000000000000 ) ;
#3904=AXIS2_PLACEMENT_3D ( 'NONE', #3496, #5120, #7329 ) ;
#3907=CIRCLE ( 'NONE', #2982, 0.7500000000001906253 ) ;
#3930=VECTOR ( 'NONE', #1959, 1000.000000000000000 ) ;
#3941=CIRCLE ( 'NONE', #5157, 0.7500000000012114754 ) ;
#3944=FACE_OUTER_BOUND ( 'NONE', #109, .T. ) ;
#3947=ADVANCED_FACE ( 'NONE', ( #1227 ), #3632, .F. ) ;
#3953=EDGE_CURVE ( 'NONE', #5769, #1000, #3581, .T. ) ;
#3958=DIRECTION ( 'NONE',  ( -1.000000000000000000, -0.000000000000000000, -0.000000000000000000 ) ) ;
#3959=VECTOR ( 'NONE', #2055, 1000.000000000000000 ) ;
#3967=ORIENTED_EDGE ( 'NONE', *, *, #6595, .F. ) ;
#3971=CARTESIAN_POINT ( 'NONE',  ( 0.000000000000000000, -7.653668647301985040, 19.22759065022772873 ) ) ;
#3978=CARTESIAN_POINT ( 'NONE',  ( 2.000000000000000000, 1.673048428422632513E-15, -13.66147716702868031 ) ) ;
#3980=ORIENTED_EDGE ( 'NONE', *, *, #7826, .T. ) ;
#3983=VERTEX_POINT ( 'NONE', #6713 ) ;
#3988=LINE ( 'NONE', #2542, #6572 ) ;
#3992=ORIENTED_EDGE ( 'NONE', *, *, #7174, .F. ) ;
#3994=EDGE_CURVE ( 'NONE', #1000, #1522, #5843, .T. ) ;
#4014=EDGE_LOOP ( 'NONE', ( #1223, #5378 ) ) ;
#4021=FACE_OUTER_BOUND ( 'NONE', #6589, .T. ) ;
#4025=ORIENTED_EDGE ( 'NONE', *, *, #343, .F. ) ;
#4038=DIRECTION ( 'NONE',  ( 1.000000000000000000, 0.000000000000000000, 0.000000000000000000 ) ) ;
#4041=CARTESIAN_POINT ( 'NONE',  ( 5.000000000000000000, 18.47759065022580316, -7.653668647301631545 ) ) ;
#4044=ADVANCED_FACE ( 'NONE', ( #839 ), #3773, .F. ) ;
#4049=DIRECTION ( 'NONE',  ( 0.000000000000000000, 0.000000000000000000, -1.000000000000000000 ) ) ;
#4062=CARTESIAN_POINT ( 'NONE',  ( 4.000000000000000000, -7.653668647301985040, 18.47759065022880520 ) ) ;
#4066=EDGE_CURVE ( 'NONE', #4647, #4346, #7683, .T. ) ;
#4071=DIRECTION ( 'NONE',  ( 0.000000000000000000, 0.000000000000000000, -1.000000000000000000 ) ) ;
#4085=CIRCLE ( 'NONE', #8830, 1.560000000002327303 ) ;
#4088=CARTESIAN_POINT ( 'NONE',  ( 3.499999999999999556, 2.755455298081544778E-15, -22.50000000000000000 ) ) ;
#4089=ORIENTED_EDGE ( 'NONE', *, *, #7837, .T. ) ;
#4105=FACE_BOUND ( 'NONE', #8366, .T. ) ;
#4106=TOROIDAL_SURFACE ( 'NONE', #7637, 15.66147716702868209, 2.000000000000000000 ) ;
#4107=FACE_OUTER_BOUND ( 'NONE', #1861, .T. ) ;
#4109=DIRECTION ( 'NONE',  ( 1.000000000000000000, 0.000000000000000000, 0.000000000000000000 ) ) ;
#4110=CIRCLE ( 'NONE', #3647, 0.7500000000013675727 ) ;
#4114=ORIENTED_EDGE ( 'NONE', *, *, #3140, .T. ) ;
#4119=DIRECTION ( 'NONE',  ( -1.000000000000000000, -0.000000000000000000, -0.000000000000000000 ) ) ;
#4125=DIRECTION ( 'NONE',  ( 0.000000000000000000, 0.000000000000000000, -1.000000000000000000 ) ) ;
#4126=CIRCLE ( 'NONE', #3207, 0.7499999999989250821 ) ;
#4129=ORIENTED_EDGE ( 'NONE', *, *, #4168, .T. ) ;
#4135=LINE ( 'NONE', #6446, #7433 ) ;
#4140=VERTEX_POINT ( 'NONE', #7758 ) ;
#4148=ORIENTED_EDGE ( 'NONE', *, *, #7924, .T. ) ;
#4149=VERTEX_POINT ( 'NONE', #3338 ) ;
#4152=CARTESIAN_POINT ( 'NONE',  ( 4.000000000000000000, 6.938893903907240211E-16, 0.000000000000000000 ) ) ;
#4159=VERTEX_POINT ( 'NONE', #1897 ) ;
#4168=EDGE_CURVE ( 'NONE', #7251, #1024, #7991, .T. ) ;
#4169=CARTESIAN_POINT ( 'NONE',  ( 4.000000000000000888, 0.000000000000000000, 17.50000000000000000 ) ) ;
#4180=CONICAL_SURFACE ( 'NONE', #2505, 22.00000000000000711, 0.7853981633974482790 ) ;
#4188=DIRECTION ( 'NONE',  ( 0.000000000000000000, 0.000000000000000000, 1.000000000000000000 ) ) ;
#4189=FACE_BOUND ( 'NONE', #5493, .T. ) ;
#4190=ORIENTED_EDGE ( 'NONE', *, *, #8035, .T. ) ;
#4191=ORIENTED_EDGE ( 'NONE', *, *, #1126, .F. ) ;
#4203=EDGE_LOOP ( 'NONE', ( #3790, #1547, #7369, #1460 ) ) ;
#4204=DIRECTION ( 'NONE',  ( -1.000000000000000000, 0.000000000000000000, 0.000000000000000000 ) ) ;
#4209=EDGE_CURVE ( 'NONE', #2688, #3554, #1860, .T. ) ;
#4215=DIRECTION ( 'NONE',  ( -1.000000000000000000, -0.000000000000000000, -0.000000000000000000 ) ) ;
#4221=DIRECTION ( 'NONE',  ( -1.000000000000000000, 0.000000000000000000, 0.000000000000000000 ) ) ;
#4226=ORIENTED_EDGE ( 'NONE', *, *, #4882, .T. ) ;
#4227=ORIENTED_EDGE ( 'NONE', *, *, #1362, .T. ) ;
#4243=CARTESIAN_POINT ( 'NONE',  ( 4.000000000000000000, 14.14213562373247868, 15.70213562373191962 ) ) ;
#4250=EDGE_LOOP ( 'NONE', ( #1737, #6781, #5977, #995 ) ) ;
#4270=ORIENTED_EDGE ( 'NONE', *, *, #6007, .T. ) ;
#4276=AXIS2_PLACEMENT_3D ( 'NONE', #6742, #725, #1394 ) ;
#4283=ORIENTED_EDGE ( 'NONE', *, *, #3281, .T. ) ;
#4284=CONICAL_SURFACE ( 'NONE', #6583, 22.50000000000000000, 0.7853981633974447263 ) ;
#4288=CARTESIAN_POINT ( 'NONE',  ( 2.000000000000000000, 0.000000000000000000, 0.000000000000000000 ) ) ;
#4294=EDGE_CURVE ( 'NONE', #4348, #5740, #5510, .T. ) ;
#4302=EDGE_LOOP ( 'NONE', ( #7977, #3992 ) ) ;
#4305=EDGE_LOOP ( 'NONE', ( #2632, #7489 ) ) ;
#4306=DIRECTION ( 'NONE',  ( 1.000000000000000000, 0.000000000000000000, 0.000000000000000000 ) ) ;
#4309=DIRECTION ( 'NONE',  ( 0.000000000000000000, 0.000000000000000000, 1.000000000000000000 ) ) ;
#4313=FACE_OUTER_BOUND ( 'NONE', #6485, .T. ) ;
#4317=DIRECTION ( 'NONE',  ( 0.000000000000000000, 0.000000000000000000, 1.000000000000000000 ) ) ;
#4328=ORIENTED_EDGE ( 'NONE', *, *, #3412, .T. ) ;
#4336=FACE_BOUND ( 'NONE', #526, .T. ) ;
#4346=VERTEX_POINT ( 'NONE', #3570 ) ;
#4348=VERTEX_POINT ( 'NONE', #4243 ) ;
#4353=CARTESIAN_POINT ( 'NONE',  ( 0.000000000000000000, 0.000000000000000000, 17.50000000000000000 ) ) ;
#4360=ADVANCED_FACE ( 'NONE', ( #2038 ), #3427, .F. ) ;
#4369=ORIENTED_EDGE ( 'NONE', *, *, #8062, .F. ) ;
#4376=CARTESIAN_POINT ( 'NONE',  ( 5.000000000000000000, -7.653668647303860872, -17.72759065022311731 ) ) ;
#4379=DIRECTION ( 'NONE',  ( -1.000000000000000000, 0.000000000000000000, -0.000000000000000000 ) ) ;
#4384=FACE_OUTER_BOUND ( 'NONE', #4553, .T. ) ;
#4391=ORIENTED_EDGE ( 'NONE', *, *, #8852, .T. ) ;
#4394=CARTESIAN_POINT ( 'NONE',  ( 4.000000000000000000, -20.00000000000120437, 2.661998082081668380E-12 ) ) ;
#4402=CARTESIAN_POINT ( 'NONE',  ( 0.000000000000000000, 7.653668647300657213, -18.47759065022568237 ) ) ;
#4419=UNCERTAINTY_MEASURE_WITH_UNIT (LENGTH_MEASURE( 1.000000000000000082E-05 ), #1594, 'distance_accuracy_value', 'NONE');
#4423=ORIENTED_EDGE ( 'NONE', *, *, #6737, .F. ) ;
#4436=VECTOR ( 'NONE', #5154, 1000.000000000000000 ) ;
#4440=CARTESIAN_POINT ( 'NONE',  ( 4.000000000000000000, 18.47759065022580316, -7.653668647301631545 ) ) ;
#4444=CARTESIAN_POINT ( 'NONE',  ( 4.000000000000000000, 2.724839128102860991E-15, -22.00000000000000355 ) ) ;
#4453=CARTESIAN_POINT ( 'NONE',  ( 3.499999999999999556, 0.000000000000000000, 0.000000000000000000 ) ) ;
#4456=EDGE_CURVE ( 'NONE', #4348, #6332, #3666, .T. ) ;
#4467=ORIENTED_EDGE ( 'NONE', *, *, #4294, .T. ) ;
#4473=DIRECTION ( 'NONE',  ( 0.000000000000000000, 0.000000000000000000, 1.000000000000000000 ) ) ;
#4477=DIRECTION ( 'NONE',  ( -1.000000000000000000, -0.000000000000000000, -0.000000000000000000 ) ) ;
#4482=DIRECTION ( 'NONE',  ( 1.000000000000000000, 0.000000000000000000, 0.000000000000000000 ) ) ;
#4485=ORIENTED_EDGE ( 'NONE', *, *, #4551, .F. ) ;
#4488=AXIS2_PLACEMENT_3D ( 'NONE', #2938, #5923, #1598 ) ;
#4497=CYLINDRICAL_SURFACE ( 'NONE', #1037, 0.7500000000013684609 ) ;
#4498=VERTEX_POINT ( 'NONE', #5926 ) ;
#4509=ADVANCED_FACE ( 'NONE', ( #8759 ), #4284, .T. ) ;
#4510=EDGE_LOOP ( 'NONE', ( #5631, #591 ) ) ;
#4518=EDGE_CURVE ( 'NONE', #9037, #8187, #69, .T. ) ;
#4529=CARTESIAN_POINT ( 'NONE',  ( 4.000000000000000000, 14.14213562373247868, 14.14213562373282329 ) ) ;
#4539=DIRECTION ( 'NONE',  ( 1.000000000000000000, 0.000000000000000000, 0.000000000000000000 ) ) ;
#4543=CARTESIAN_POINT ( 'NONE',  ( 4.000000000000000000, 20.00000000000120437, -1.559999999998198161 ) ) ;
#4550=CARTESIAN_POINT ( 'NONE',  ( 4.000000000000000000, 7.653668647300657213, -19.22759065022689384 ) ) ;
#4551=EDGE_CURVE ( 'NONE', #5692, #8610, #9030, .T. ) ;
#4553=EDGE_LOOP ( 'NONE', ( #9025, #3094, #4129, #8159 ) ) ;
#4556=DIRECTION ( 'NONE',  ( 0.000000000000000000, 0.000000000000000000, 1.000000000000000000 ) ) ;
#4565=VERTEX_POINT ( 'NONE', #5306 ) ;
#4571=CARTESIAN_POINT ( 'NONE',  ( 4.000000000000000000, 14.14213562373112154, -15.70213562373078098 ) ) ;
#4572=AXIS2_PLACEMENT_3D ( 'NONE', #2007, #7190, #6248 ) ;
#4573=LINE ( 'NONE', #3033, #8475 ) ;
#4583=FACE_OUTER_BOUND ( 'NONE', #6851, .T. ) ;
#4584=CARTESIAN_POINT ( 'NONE',  ( 5.000000000000000000, -7.653668647303860872, -19.22759065022669134 ) ) ;
#4586=CIRCLE ( 'NONE', #439, 0.7500000000017874591 ) ;
#4591=EDGE_LOOP ( 'NONE', ( #4969, #8488, #6750, #4191 ) ) ;
#4592=CARTESIAN_POINT ( 'NONE',  ( 0.000000000000000000, 18.47759065022580316, -8.403668647301632433 ) ) ;
#4594=VECTOR ( 'NONE', #5871, 1000.000000000000000 ) ;
#4598=DIRECTION ( 'NONE',  ( -1.000000000000000000, -0.000000000000000000, -0.000000000000000000 ) ) ;
#4603=EDGE_LOOP ( 'NONE', ( #4369, #1748 ) ) ;
#4605=ORIENTED_EDGE ( 'NONE', *, *, #3953, .F. ) ;
#4608=ORIENTED_EDGE ( 'NONE', *, *, #5261, .T. ) ;
#4620=FACE_OUTER_BOUND ( 'NONE', #8645, .T. ) ;
#4624=CARTESIAN_POINT ( 'NONE',  ( 5.000000000000000000, -7.653668647303860872, -18.47759065022490432 ) ) ;
#4626=ADVANCED_BREP_SHAPE_REPRESENTATION ( '', ( #190, #1614 ), #7287 ) ;
#4645=AXIS2_PLACEMENT_3D ( 'NONE', #4440, #7263, #7311 ) ;
#4647=VERTEX_POINT ( 'NONE', #2517 ) ;
#4650=ORIENTED_EDGE ( 'NONE', *, *, #711, .F. ) ;
#4653=AXIS2_PLACEMENT_3D ( 'NONE', #6368, #7170, #1357 ) ;
#4674=( NAMED_UNIT ( * ) SI_UNIT ( $, .STERADIAN. ) SOLID_ANGLE_UNIT ( ) );
#4695=VERTEX_POINT ( 'NONE', #4728 ) ;
#4701=ORIENTED_EDGE ( 'NONE', *, *, #9139, .T. ) ;
#4702=CIRCLE ( 'NONE', #5625, 13.66147716702868031 ) ;
#4706=AXIS2_PLACEMENT_3D ( 'NONE', #3334, #3286, #2577 ) ;
#4710=ADVANCED_FACE ( 'NONE', ( #7601 ), #6127, .F. ) ;
#4712=CIRCLE ( 'NONE', #5173, 1.560000000000000719 ) ;
#4727=AXIS2_PLACEMENT_3D ( 'NONE', #6575, #3684, #7235 ) ;
#4728=CARTESIAN_POINT ( 'NONE',  ( 0.000000000000000000, 18.47759065022658120, 8.403668647301545391 ) ) ;
#4730=DIRECTION ( 'NONE',  ( -1.000000000000000000, -0.000000000000000000, -0.000000000000000000 ) ) ;
#4733=VECTOR ( 'NONE', #8675, 1000.000000000000000 ) ;
#4738=ADVANCED_FACE ( 'NONE', ( #9321 ), #7072, .F. ) ;
#4770=ORIENTED_EDGE ( 'NONE', *, *, #1850, .T. ) ;
#4774=EDGE_CURVE ( 'NONE', #6226, #7541, #5511, .T. ) ;
#4783=CARTESIAN_POINT ( 'NONE',  ( 0.000000000000000000, -7.653668647303860872, -19.22759065022669134 ) ) ;
#4793=CIRCLE ( 'NONE', #1873, 1.560000000000134168 ) ;
#4801=DIRECTION ( 'NONE',  ( -1.000000000000000000, 0.000000000000000000, 0.000000000000000000 ) ) ;
#4809=DIRECTION ( 'NONE',  ( 1.000000000000000000, 0.000000000000000000, 0.000000000000000000 ) ) ;
#4814=LINE ( 'NONE', #5591, #5244 ) ;
#4816=DIRECTION ( 'NONE',  ( 0.000000000000000000, 0.000000000000000000, 1.000000000000000000 ) ) ;
#4821=FACE_BOUND ( 'NONE', #604, .T. ) ;
#4838=VERTEX_POINT ( 'NONE', #1249 ) ;
#4841=CIRCLE ( 'NONE', #5008, 0.7500000000001906253 ) ;
#4848=ORIENTED_EDGE ( 'NONE', *, *, #4294, .F. ) ;
#4850=DIRECTION ( 'NONE',  ( 0.000000000000000000, 0.000000000000000000, 1.000000000000000000 ) ) ;
#4855=EDGE_LOOP ( 'NONE', ( #9434, #7832, #5773, #7104 ) ) ;
#4863=AXIS2_PLACEMENT_3D ( 'NONE', #2940, #3716, #6648 ) ;
#4868=DIRECTION ( 'NONE',  ( -1.000000000000000000, -0.000000000000000000, -0.000000000000000000 ) ) ;
#4875=DIRECTION ( 'NONE',  ( -1.000000000000000000, 0.000000000000000000, 0.000000000000000000 ) ) ;
#4876=CYLINDRICAL_SURFACE ( 'NONE', #59, 1.560000000002236709 ) ;
#4877=ORIENTED_EDGE ( 'NONE', *, *, #6002, .F. ) ;
#4882=EDGE_CURVE ( 'NONE', #2987, #8436, #8838, .T. ) ;
#4901=ORIENTED_EDGE ( 'NONE', *, *, #8035, .F. ) ;
#4902=ORIENTED_EDGE ( 'NONE', *, *, #3599, .F. ) ;
#4903=VERTEX_POINT ( 'NONE', #5868 ) ;
#4907=DIRECTION ( 'NONE',  ( -1.000000000000000000, 0.000000000000000000, 0.000000000000000000 ) ) ;
#4908=DIRECTION ( 'NONE',  ( -1.000000000000000000, -0.000000000000000000, -0.000000000000000000 ) ) ;
#4909=DIRECTION ( 'NONE',  ( -1.000000000000000000, -0.000000000000000000, -0.000000000000000000 ) ) ;
#4910=VERTEX_POINT ( 'NONE', #811 ) ;
#4916=ADVANCED_FACE ( 'NONE', ( #5820 ), #8791, .F. ) ;
#4943=EDGE_CURVE ( 'NONE', #6332, #4348, #143, .T. ) ;
#4946=ORIENTED_EDGE ( 'NONE', *, *, #4518, .T. ) ;
#4956=EDGE_CURVE ( 'NONE', #4498, #2916, #1822, .T. ) ;
#4957=CYLINDRICAL_SURFACE ( 'NONE', #8245, 17.50000000000000000 ) ;
#4961=ORIENTED_EDGE ( 'NONE', *, *, #1735, .F. ) ;
#4962=FACE_BOUND ( 'NONE', #4014, .T. ) ;
#4966=DIRECTION ( 'NONE',  ( 0.000000000000000000, 0.000000000000000000, -1.000000000000000000 ) ) ;
#4969=ORIENTED_EDGE ( 'NONE', *, *, #1525, .T. ) ;
#4975=DIRECTION ( 'NONE',  ( 0.000000000000000000, 0.000000000000000000, -1.000000000000000000 ) ) ;
#4985=ORIENTED_EDGE ( 'NONE', *, *, #2850, .F. ) ;
#5004=DIRECTION ( 'NONE',  ( 0.000000000000000000, 0.000000000000000000, 1.000000000000000000 ) ) ;
#5008=AXIS2_PLACEMENT_3D ( 'NONE', #6997, #460, #2725 ) ;
#5010=EDGE_CURVE ( 'NONE', #9366, #1900, #2218, .T. ) ;
#5013=CARTESIAN_POINT ( 'NONE',  ( 0.000000000000000000, 0.000000000000000000, 0.000000000000000000 ) ) ;
#5021=ORIENTED_EDGE ( 'NONE', *, *, #700, .T. ) ;
#5022=AXIS2_PLACEMENT_3D ( 'NONE', #5906, #7975, #1385 ) ;
#5037=EDGE_LOOP ( 'NONE', ( #1145, #1328, #8691, #1378 ) ) ;
#5038=ORIENTED_EDGE ( 'NONE', *, *, #6777, .T. ) ;
#5039=CIRCLE ( 'NONE', #286, 13.66147716702868031 ) ;
#5040=DIRECTION ( 'NONE',  ( 0.000000000000000000, 0.000000000000000000, 1.000000000000000000 ) ) ;
#5045=DIRECTION ( 'NONE',  ( 0.000000000000000000, 0.000000000000000000, 1.000000000000000000 ) ) ;
#5048=ADVANCED_FACE ( 'NONE', ( #7547 ), #5347, .F. ) ;
#5049=ORIENTED_EDGE ( 'NONE', *, *, #2739, .T. ) ;
#5056=CARTESIAN_POINT ( 'NONE',  ( 0.000000000000000000, -7.653668647301985040, 18.47759065022880520 ) ) ;
#5062=DIRECTION ( 'NONE',  ( 0.000000000000000000, 0.000000000000000000, 1.000000000000000000 ) ) ;
#5068=VERTEX_POINT ( 'NONE', #5483 ) ;
#5078=CARTESIAN_POINT ( 'NONE',  ( 0.000000000000000000, 7.653668647300657213, -19.22759065022689384 ) ) ;
#5087=VERTEX_POINT ( 'NONE', #4571 ) ;
#5105=FACE_OUTER_BOUND ( 'NONE', #9338, .T. ) ;
#5106=DIRECTION ( 'NONE',  ( -1.000000000000000000, -0.000000000000000000, -0.000000000000000000 ) ) ;
#5115=CARTESIAN_POINT ( 'NONE',  ( 3.499999999999999556, 0.000000000000000000, 22.50000000000000000 ) ) ;
#5117=EDGE_CURVE ( 'NONE', #5750, #1024, #3267, .T. ) ;
#5120=DIRECTION ( 'NONE',  ( -1.000000000000000000, 0.000000000000000000, 0.000000000000000000 ) ) ;
#5127=LINE ( 'NONE', #2966, #6117 ) ;
#5143=CARTESIAN_POINT ( 'NONE',  ( 4.000000000000000000, -14.14213562373112154, 14.14213562373418220 ) ) ;
#5145=CARTESIAN_POINT ( 'NONE',  ( 5.000000000000000000, 18.47759065022658120, 7.653668647302884764 ) ) ;
#5148=EDGE_LOOP ( 'NONE', ( #73, #588 ) ) ;
#5154=DIRECTION ( 'NONE',  ( -1.000000000000000000, -0.000000000000000000, -0.000000000000000000 ) ) ;
#5155=EDGE_CURVE ( 'NONE', #1835, #8069, #4135, .T. ) ;
#5156=CARTESIAN_POINT ( 'NONE',  ( 5.000000000000000000, -14.14213562373248401, -12.58213562372718641 ) ) ;
#5157=AXIS2_PLACEMENT_3D ( 'NONE', #697, #5616, #9246 ) ;
#5162=ORIENTED_EDGE ( 'NONE', *, *, #1023, .F. ) ;
#5166=DIRECTION ( 'NONE',  ( 0.000000000000000000, 0.000000000000000000, 1.000000000000000000 ) ) ;
#5169=FACE_OUTER_BOUND ( 'NONE', #2325, .T. ) ;
#5171=DIRECTION ( 'NONE',  ( 1.000000000000000000, 0.000000000000000000, 0.000000000000000000 ) ) ;
#5173=AXIS2_PLACEMENT_3D ( 'NONE', #1840, #7554, #2422 ) ;
#5175=EDGE_LOOP ( 'NONE', ( #5162, #8623 ) ) ;
#5184=DIRECTION ( 'NONE',  ( 0.000000000000000000, 0.000000000000000000, 1.000000000000000000 ) ) ;
#5189=ORIENTED_EDGE ( 'NONE', *, *, #427, .F. ) ;
#5191=AXIS2_PLACEMENT_3D ( 'NONE', #787, #3628, #5988 ) ;
#5199=CIRCLE ( 'NONE', #1201, 0.7499999999989250821 ) ;
#5209=EDGE_LOOP ( 'NONE', ( #6848, #8598, #4467, #6349 ) ) ;
#5214=DIRECTION ( 'NONE',  ( 1.000000000000000000, 0.000000000000000000, 0.000000000000000000 ) ) ;
#5222=DIRECTION ( 'NONE',  ( 0.000000000000000000, 0.000000000000000000, 1.000000000000000000 ) ) ;
#5233=CARTESIAN_POINT ( 'NONE',  ( 0.000000000000000000, 18.47759065022580316, -6.903668647301629768 ) ) ;
#5242=EDGE_CURVE ( 'NONE', #7405, #3020, #2746, .T. ) ;
#5244=VECTOR ( 'NONE', #8472, 1000.000000000000000 ) ;
#5247=CYLINDRICAL_SURFACE ( 'NONE', #447, 1.560000000001265263 ) ;
#5255=DIRECTION ( 'NONE',  ( -1.000000000000000000, -0.000000000000000000, -0.000000000000000000 ) ) ;
#5259=DIRECTION ( 'NONE',  ( 0.000000000000000000, 0.000000000000000000, -1.000000000000000000 ) ) ;
#5260=LINE ( 'NONE', #5156, #3862 ) ;
#5261=EDGE_CURVE ( 'NONE', #1522, #1000, #5605, .T. ) ;
#5267=VERTEX_POINT ( 'NONE', #750 ) ;
#5290=CARTESIAN_POINT ( 'NONE',  ( 0.000000000000000000, -14.14213562373248401, -15.70213562373165850 ) ) ;
#5306=CARTESIAN_POINT ( 'NONE',  ( 4.000000000000000000, 9.603694566548697359E-13, 21.56000000000303984 ) ) ;
#5307=DIRECTION ( 'NONE',  ( -1.000000000000000000, 0.000000000000000000, 0.000000000000000000 ) ) ;
#5313=DIRECTION ( 'NONE',  ( 0.000000000000000000, 0.000000000000000000, 1.000000000000000000 ) ) ;
#5334=AXIS2_PLACEMENT_3D ( 'NONE', #7990, #5255, #5062 ) ;
#5335=CARTESIAN_POINT ( 'NONE',  ( 0.000000000000000000, 0.000000000000000000, 13.66147716702868031 ) ) ;
#5343=VECTOR ( 'NONE', #8310, 1000.000000000000000 ) ;
#5347=CYLINDRICAL_SURFACE ( 'NONE', #2986, 1.560000000001265263 ) ;
#5348=EDGE_CURVE ( 'NONE', #694, #7436, #8351, .T. ) ;
#5350=CYLINDRICAL_SURFACE ( 'NONE', #6111, 0.7500000000001915135 ) ;
#5357=DIRECTION ( 'NONE',  ( 0.000000000000000000, 0.000000000000000000, 1.000000000000000000 ) ) ;
#5370=VECTOR ( 'NONE', #2981, 1000.000000000000000 ) ;
#5378=ORIENTED_EDGE ( 'NONE', *, *, #6250, .F. ) ;
#5401=DIRECTION ( 'NONE',  ( -1.000000000000000000, -0.000000000000000000, -0.000000000000000000 ) ) ;
#5403=ORIENTED_EDGE ( 'NONE', *, *, #3709, .F. ) ;
#5407=EDGE_LOOP ( 'NONE', ( #6471, #6988 ) ) ;
#5413=CIRCLE ( 'NONE', #8481, 0.7500000000013675727 ) ;
#5436=LINE ( 'NONE', #202, #5343 ) ;
#5447=AXIS2_PLACEMENT_3D ( 'NONE', #3619, #5700, #3472 ) ;
#5450=CARTESIAN_POINT ( 'NONE',  ( 5.000000000000000000, -14.14213562373112154, 12.58213562373271621 ) ) ;
#5459=ADVANCED_FACE ( 'NONE', ( #5169 ), #1755, .T. ) ;
#5464=LINE ( 'NONE', #7474, #812 ) ;
#5476=VERTEX_POINT ( 'NONE', #1124 ) ;
#5483=CARTESIAN_POINT ( 'NONE',  ( 19.00000000000000000, 0.000000000000000000, 17.50000000000000000 ) ) ;
#5489=AXIS2_PLACEMENT_3D ( 'NONE', #8684, #2100, #7971 ) ;
#5493=EDGE_LOOP ( 'NONE', ( #452, #7779 ) ) ;
#5496=CYLINDRICAL_SURFACE ( 'NONE', #7016, 1.559999999999096776 ) ;
#5497=VECTOR ( 'NONE', #1422, 1000.000000000000000 ) ;
#5504=DIRECTION ( 'NONE',  ( 0.000000000000000000, 0.000000000000000000, 1.000000000000000000 ) ) ;
#5509=CIRCLE ( 'NONE', #6740, 1.559999999999096776 ) ;
#5510=LINE ( 'NONE', #9333, #7689 ) ;
#5511=CIRCLE ( 'NONE', #6452, 1.559999999998939346 ) ;
#5516=FACE_OUTER_BOUND ( 'NONE', #9285, .T. ) ;
#5521=EDGE_CURVE ( 'NONE', #8998, #23, #5598, .T. ) ;
#5532=CARTESIAN_POINT ( 'NONE',  ( 4.000000000000000000, 14.14213562373247868, 12.58213562373372341 ) ) ;
#5550=ORIENTED_EDGE ( 'NONE', *, *, #2557, .T. ) ;
#5554=FACE_BOUND ( 'NONE', #1289, .T. ) ;
#5560=AXIS2_PLACEMENT_3D ( 'NONE', #4288, #4908, #5780 ) ;
#5582=LINE ( 'NONE', #1149, #7019 ) ;
#5591=CARTESIAN_POINT ( 'NONE',  ( 5.000000000000000000, -18.47759065022790637, -6.903668647298391470 ) ) ;
#5593=CIRCLE ( 'NONE', #3287, 1.560000000000134168 ) ;
#5598=CIRCLE ( 'NONE', #1917, 1.560000000002236709 ) ;
#5600=FACE_BOUND ( 'NONE', #2420, .T. ) ;
#5605=CIRCLE ( 'NONE', #3904, 0.7500000000000015543 ) ;
#5612=CARTESIAN_POINT ( 'NONE',  ( 0.000000000000000000, 9.603694566548697359E-13, 21.56000000000303984 ) ) ;
#5616=DIRECTION ( 'NONE',  ( 1.000000000000000000, 0.000000000000000000, 0.000000000000000000 ) ) ;
#5625=AXIS2_PLACEMENT_3D ( 'NONE', #7136, #557, #4309 ) ;
#5630=ADVANCED_FACE ( 'NONE', ( #8761 ), #72, .T. ) ;
#5631=ORIENTED_EDGE ( 'NONE', *, *, #8243, .F. ) ;
#5634=CIRCLE ( 'NONE', #5783, 0.7499999999986606269 ) ;
#5635=CARTESIAN_POINT ( 'NONE',  ( 19.00000000000000000, 2.143131898507868248E-15, -17.50000000000000000 ) ) ;
#5640=CIRCLE ( 'NONE', #5489, 0.7500000000017874591 ) ;
#5642=FACE_BOUND ( 'NONE', #4305, .T. ) ;
#5651=CARTESIAN_POINT ( 'NONE',  ( 5.000000000000000000, 9.603694566548697359E-13, 20.00000000000290612 ) ) ;
#5653=CARTESIAN_POINT ( 'NONE',  ( 3.499999999999999556, 0.000000000000000000, 0.000000000000000000 ) ) ;
#5665=CARTESIAN_POINT ( 'NONE',  ( 5.000000000000000000, 7.653668647300657213, -19.22759065022689384 ) ) ;
#5666=EDGE_CURVE ( 'NONE', #2437, #8069, #7891, .T. ) ;
#5673=EDGE_CURVE ( 'NONE', #2622, #6180, #7897, .T. ) ;
#5678=DIRECTION ( 'NONE',  ( -1.000000000000000000, -0.000000000000000000, -0.000000000000000000 ) ) ;
#5684=EDGE_LOOP ( 'NONE', ( #4605, #3050, #8085, #4608 ) ) ;
#5686=DIRECTION ( 'NONE',  ( -1.000000000000000000, -0.000000000000000000, -0.000000000000000000 ) ) ;
#5690=FACE_BOUND ( 'NONE', #1712, .T. ) ;
#5692=VERTEX_POINT ( 'NONE', #8038 ) ;
#5697=EDGE_CURVE ( 'NONE', #9340, #5087, #7853, .T. ) ;
#5700=DIRECTION ( 'NONE',  ( -1.000000000000000000, -0.000000000000000000, -0.000000000000000000 ) ) ;
#5709=VECTOR ( 'NONE', #4730, 1000.000000000000000 ) ;
#5718=EDGE_CURVE ( 'NONE', #5068, #7405, #2790, .T. ) ;
#5730=EDGE_CURVE ( 'NONE', #3148, #5750, #3247, .T. ) ;
#5733=CARTESIAN_POINT ( 'NONE',  ( 5.000000000000000000, -20.00000000000120437, -1.559999999999665432 ) ) ;
#5738=FACE_BOUND ( 'NONE', #4510, .T. ) ;
#5740=VERTEX_POINT ( 'NONE', #928 ) ;
#5743=FACE_BOUND ( 'NONE', #4603, .T. ) ;
#5745=CYLINDRICAL_SURFACE ( 'NONE', #9461, 22.50000000000000000 ) ;
#5747=DIRECTION ( 'NONE',  ( 1.000000000000000000, 0.000000000000000000, 0.000000000000000000 ) ) ;
#5750=VERTEX_POINT ( 'NONE', #8092 ) ;
#5751=CARTESIAN_POINT ( 'NONE',  ( 5.000000000000000000, -18.47759065022790637, -8.403668647301127947 ) ) ;
#5753=EDGE_CURVE ( 'NONE', #694, #23, #5260, .T. ) ;
#5762=DIRECTION ( 'NONE',  ( 1.000000000000000000, 0.000000000000000000, 0.000000000000000000 ) ) ;
#5764=VERTEX_POINT ( 'NONE', #4444 ) ;
#5769=VERTEX_POINT ( 'NONE', #6080 ) ;
#5771=ORIENTED_EDGE ( 'NONE', *, *, #5697, .T. ) ;
#5773=ORIENTED_EDGE ( 'NONE', *, *, #7109, .T. ) ;
#5778=CARTESIAN_POINT ( 'NONE',  ( 5.000000000000000000, -18.47759065022790637, -7.653668647299759265 ) ) ;
#5780=DIRECTION ( 'NONE',  ( 0.000000000000000000, 0.000000000000000000, 1.000000000000000000 ) ) ;
#5783=AXIS2_PLACEMENT_3D ( 'NONE', #2230, #2954, #5166 ) ;
#5785=ORIENTED_EDGE ( 'NONE', *, *, #6131, .F. ) ;
#5786=CARTESIAN_POINT ( 'NONE',  ( 5.000000000000000000, 18.47759065022658120, 7.653668647302884764 ) ) ;
#5788=AXIS2_PLACEMENT_3D ( 'NONE', #5786, #8713, #2131 ) ;
#5797=CARTESIAN_POINT ( 'NONE',  ( 0.000000000000000000, -7.653668647301985040, 18.47759065022880520 ) ) ;
#5803=DIRECTION ( 'NONE',  ( -1.000000000000000000, 0.000000000000000000, 0.000000000000000000 ) ) ;
#5816=VECTOR ( 'NONE', #7644, 1000.000000000000000 ) ;
#5820=FACE_OUTER_BOUND ( 'NONE', #618, .T. ) ;
#5825=FACE_BOUND ( 'NONE', #8621, .T. ) ;
#5835=DIRECTION ( 'NONE',  ( 0.000000000000000000, 0.000000000000000000, 1.000000000000000000 ) ) ;
#5837=ORIENTED_EDGE ( 'NONE', *, *, #1428, .T. ) ;
#5841=DIRECTION ( 'NONE',  ( 1.000000000000000000, 0.000000000000000000, 0.000000000000000000 ) ) ;
#5843=CIRCLE ( 'NONE', #1383, 0.7500000000000015543 ) ;
#5848=DIRECTION ( 'NONE',  ( 1.000000000000000000, 0.000000000000000000, 0.000000000000000000 ) ) ;
#5853=DIRECTION ( 'NONE',  ( -1.000000000000000000, -0.000000000000000000, -0.000000000000000000 ) ) ;
#5858=DIRECTION ( 'NONE',  ( 1.000000000000000000, 0.000000000000000000, 0.000000000000000000 ) ) ;
#5865=EDGE_CURVE ( 'NONE', #4910, #1656, #8311, .T. ) ;
#5868=CARTESIAN_POINT ( 'NONE',  ( 2.000000000000000000, 0.000000000000000000, 13.66147716702868031 ) ) ;
#5871=DIRECTION ( 'NONE',  ( -1.000000000000000000, -0.000000000000000000, -0.000000000000000000 ) ) ;
#5878=CYLINDRICAL_SURFACE ( 'NONE', #5334, 1.559999999998939346 ) ;
#5899=DIRECTION ( 'NONE',  ( -1.000000000000000000, -0.000000000000000000, -0.000000000000000000 ) ) ;
#5906=CARTESIAN_POINT ( 'NONE',  ( 5.000000000000000000, 7.653668647300657213, -18.47759065022568237 ) ) ;
#5907=ORIENTED_EDGE ( 'NONE', *, *, #7403, .T. ) ;
#5909=VECTOR ( 'NONE', #4119, 1000.000000000000000 ) ;
#5914=FACE_OUTER_BOUND ( 'NONE', #2862, .T. ) ;
#5920=DIRECTION ( 'NONE',  ( 0.000000000000000000, 0.000000000000000000, 1.000000000000000000 ) ) ;
#5923=DIRECTION ( 'NONE',  ( -1.000000000000000000, -0.000000000000000000, -0.000000000000000000 ) ) ;
#5924=EDGE_CURVE ( 'NONE', #4838, #4159, #4814, .T. ) ;
#5926=CARTESIAN_POINT ( 'NONE',  ( 4.000000000000000000, -14.14213562373112154, 12.58213562373271621 ) ) ;
#5945=EDGE_CURVE ( 'NONE', #3385, #7541, #7030, .T. ) ;
#5947=CIRCLE ( 'NONE', #6261, 22.00000000000000355 ) ;
#5949=ADVANCED_FACE ( 'NONE', ( #1113 ), #7602, .F. ) ;
#5954=AXIS2_PLACEMENT_3D ( 'NONE', #370, #993, #7725 ) ;
#5964=AXIS2_PLACEMENT_3D ( 'NONE', #1118, #8437, #8382 ) ;
#5969=DIRECTION ( 'NONE',  ( 1.000000000000000000, 0.000000000000000000, 0.000000000000000000 ) ) ;
#5970=CARTESIAN_POINT ( 'NONE',  ( 4.000000000000000000, 9.603694566548697359E-13, 20.00000000000290612 ) ) ;
#5971=CARTESIAN_POINT ( 'NONE',  ( 5.000000000000000000, 18.47759065022580316, -6.903668647301629768 ) ) ;
#5972=CARTESIAN_POINT ( 'NONE',  ( 4.000000000000000000, -14.14213562373248401, -14.14213562372942157 ) ) ;
#5977=ORIENTED_EDGE ( 'NONE', *, *, #4066, .T. ) ;
#5988=DIRECTION ( 'NONE',  ( 0.000000000000000000, 0.000000000000000000, 1.000000000000000000 ) ) ;
#5991=CARTESIAN_POINT ( 'NONE',  ( 4.000000000000000000, -14.14213562373112154, 14.14213562373418220 ) ) ;
#5996=EDGE_LOOP ( 'NONE', ( #312, #8506 ) ) ;
#6002=EDGE_CURVE ( 'NONE', #4498, #2113, #6129, .T. ) ;
#6007=EDGE_CURVE ( 'NONE', #4903, #2056, #1093, .T. ) ;
#6014=AXIS2_PLACEMENT_3D ( 'NONE', #5056, #3461, #4188 ) ;
#6035=CIRCLE ( 'NONE', #1884, 13.66147716702868031 ) ;
#6039=DIRECTION ( 'NONE',  ( 1.000000000000000000, 0.000000000000000000, 0.000000000000000000 ) ) ;
#6041=DIRECTION ( 'NONE',  ( 0.000000000000000000, 0.000000000000000000, -1.000000000000000000 ) ) ;
#6043=EDGE_CURVE ( 'NONE', #2947, #6912, #336, .T. ) ;
#6047=EDGE_LOOP ( 'NONE', ( #5771, #3525, #3817, #978 ) ) ;
#6052=ADVANCED_FACE ( 'NONE', ( #7886 ), #8655, .F. ) ;
#6059=ORIENTED_EDGE ( 'NONE', *, *, #6304, .T. ) ;
#6080=CARTESIAN_POINT ( 'NONE',  ( 4.000000000000000000, 18.47759065022580316, -8.403668647301632433 ) ) ;
#6084=VERTEX_POINT ( 'NONE', #7257 ) ;
#6086=CARTESIAN_POINT ( 'NONE',  ( 4.000000000000000000, -20.00000000000120437, 1.560000000004989174 ) ) ;
#6095=EDGE_LOOP ( 'NONE', ( #8883, #4114, #2992, #1847 ) ) ;
#6104=CARTESIAN_POINT ( 'NONE',  ( 0.000000000000000000, 18.47759065022658120, 6.903668647304224137 ) ) ;
#6111=AXIS2_PLACEMENT_3D ( 'NONE', #8313, #6208, #9123 ) ;
#6117=VECTOR ( 'NONE', #5899, 1000.000000000000000 ) ;
#6125=CARTESIAN_POINT ( 'NONE',  ( 0.4999999999999935052, 2.755455298081544778E-15, -22.50000000000000000 ) ) ;
#6127=CYLINDRICAL_SURFACE ( 'NONE', #1354, 1.559999999998939346 ) ;
#6129=LINE ( 'NONE', #5450, #5709 ) ;
#6131=EDGE_CURVE ( 'NONE', #3020, #2924, #485, .T. ) ;
#6143=DIRECTION ( 'NONE',  ( 0.000000000000000000, 0.000000000000000000, -1.000000000000000000 ) ) ;
#6144=DIRECTION ( 'NONE',  ( 0.000000000000000000, 0.000000000000000000, 1.000000000000000000 ) ) ;
#6147=ORIENTED_EDGE ( 'NONE', *, *, #823, .T. ) ;
#6151=ADVANCED_FACE ( 'NONE', ( #5914 ), #7498, .F. ) ;
#6174=CARTESIAN_POINT ( 'NONE',  ( 5.000000000000000000, 14.14213562373247868, 14.14213562373282329 ) ) ;
#6176=DIRECTION ( 'NONE',  ( 0.000000000000000000, 0.000000000000000000, 1.000000000000000000 ) ) ;
#6178=ORIENTED_EDGE ( 'NONE', *, *, #5673, .T. ) ;
#6180=VERTEX_POINT ( 'NONE', #159 ) ;
#6205=SHAPE_DEFINITION_REPRESENTATION ( #3703, #1625 ) ;
#6206=DIRECTION ( 'NONE',  ( 0.000000000000000000, 0.000000000000000000, 1.000000000000000000 ) ) ;
#6208=DIRECTION ( 'NONE',  ( -1.000000000000000000, -0.000000000000000000, -0.000000000000000000 ) ) ;
#6221=VECTOR ( 'NONE', #2465, 1000.000000000000114 ) ;
#6226=VERTEX_POINT ( 'NONE', #8027 ) ;
#6235=ORIENTED_EDGE ( 'NONE', *, *, #7859, .F. ) ;
#6236=ORIENTED_EDGE ( 'NONE', *, *, #3281, .F. ) ;
#6239=VERTEX_POINT ( 'NONE', #813 ) ;
#6243=CIRCLE ( 'NONE', #546, 22.00000000000000355 ) ;
#6246=EDGE_CURVE ( 'NONE', #6332, #5476, #4573, .T. ) ;
#6248=DIRECTION ( 'NONE',  ( 0.000000000000000000, 0.000000000000000000, 1.000000000000000000 ) ) ;
#6250=EDGE_CURVE ( 'NONE', #602, #4565, #4793, .T. ) ;
#6257=FACE_OUTER_BOUND ( 'NONE', #8443, .T. ) ;
#6261=AXIS2_PLACEMENT_3D ( 'NONE', #7888, #634, #2760 ) ;
#6267=EDGE_LOOP ( 'NONE', ( #8392, #9059 ) ) ;
#6277=AXIS2_PLACEMENT_3D ( 'NONE', #1872, #4801, #4850 ) ;
#6291=CARTESIAN_POINT ( 'NONE',  ( 0.000000000000000000, -9.628187502531647418E-13, -18.43999999999823913 ) ) ;
#6295=ORIENTED_EDGE ( 'NONE', *, *, #3709, .T. ) ;
#6302=ORIENTED_EDGE ( 'NONE', *, *, #6246, .T. ) ;
#6303=DIRECTION ( 'NONE',  ( 0.000000000000000000, 0.000000000000000000, -1.000000000000000000 ) ) ;
#6304=EDGE_CURVE ( 'NONE', #9386, #3367, #3558, .T. ) ;
#6320=EDGE_LOOP ( 'NONE', ( #170, #8927 ) ) ;
#6324=DIRECTION ( 'NONE',  ( 1.000000000000000000, 0.000000000000000000, 0.000000000000000000 ) ) ;
#6327=AXIS2_PLACEMENT_3D ( 'NONE', #3417, #3512, #5004 ) ;
#6332=VERTEX_POINT ( 'NONE', #5532 ) ;
#6334=CARTESIAN_POINT ( 'NONE',  ( 0.000000000000000000, 1.673048428422632513E-15, -13.66147716702868031 ) ) ;
#6349=ORIENTED_EDGE ( 'NONE', *, *, #1008, .T. ) ;
#6350=ORIENTED_EDGE ( 'NONE', *, *, #2430, .F. ) ;
#6357=CARTESIAN_POINT ( 'NONE',  ( 4.000000000000000888, 0.000000000000000000, 0.000000000000000000 ) ) ;
#6358=EDGE_CURVE ( 'NONE', #4565, #9386, #5127, .T. ) ;
#6361=DIRECTION ( 'NONE',  ( -0.000000000000000000, 0.000000000000000000, 1.000000000000000000 ) ) ;
#6368=CARTESIAN_POINT ( 'NONE',  ( 0.000000000000000000, -7.653668647303860872, -18.47759065022490432 ) ) ;
#6375=DIRECTION ( 'NONE',  ( 0.000000000000000000, 0.000000000000000000, 1.000000000000000000 ) ) ;
#6386=CARTESIAN_POINT ( 'NONE',  ( 0.000000000000000000, -7.653668647301985040, 17.72759065022987812 ) ) ;
#6402=DIRECTION ( 'NONE',  ( 0.000000000000000000, 0.000000000000000000, -1.000000000000000000 ) ) ;
#6406=AXIS2_PLACEMENT_3D ( 'NONE', #1068, #2515, #4049 ) ;
#6407=FACE_OUTER_BOUND ( 'NONE', #6959, .T. ) ;
#6412=CIRCLE ( 'NONE', #575, 1.559999999998939346 ) ;
#6413=PLANE ( 'NONE',  #8328 ) ;
#6418=DIRECTION ( 'NONE',  ( -1.000000000000000000, -0.000000000000000000, -0.000000000000000000 ) ) ;
#6425=ORIENTED_EDGE ( 'NONE', *, *, #1833, .F. ) ;
#6436=AXIS2_PLACEMENT_3D ( 'NONE', #1511, #6569, #8863 ) ;
#6446=CARTESIAN_POINT ( 'NONE',  ( 3.499999999999999556, 0.000000000000000000, 22.50000000000000000 ) ) ;
#6447=LINE ( 'NONE', #9362, #1895 ) ;
#6452=AXIS2_PLACEMENT_3D ( 'NONE', #9371, #4907, #2798 ) ;
#6459=DIRECTION ( 'NONE',  ( 0.000000000000000000, 0.000000000000000000, -1.000000000000000000 ) ) ;
#6464=DIRECTION ( 'NONE',  ( 0.000000000000000000, 0.000000000000000000, -1.000000000000000000 ) ) ;
#6465=EDGE_CURVE ( 'NONE', #3685, #4695, #9318, .T. ) ;
#6471=ORIENTED_EDGE ( 'NONE', *, *, #4209, .F. ) ;
#6473=CARTESIAN_POINT ( 'NONE',  ( 0.000000000000000000, 7.653668647300657213, -17.72759065022447089 ) ) ;
#6476=CARTESIAN_POINT ( 'NONE',  ( 19.00000000000000000, 0.000000000000000000, 0.000000000000000000 ) ) ;
#6485=EDGE_LOOP ( 'NONE', ( #3967, #8493, #5049, #4270 ) ) ;
#6494=VERTEX_POINT ( 'NONE', #6958 ) ;
#6510=CARTESIAN_POINT ( 'NONE',  ( 19.00000000000000000, 0.000000000000000000, 0.000000000000000000 ) ) ;
#6523=CARTESIAN_POINT ( 'NONE',  ( 4.000000000000000000, 18.47759065022658120, 7.653668647302884764 ) ) ;
#6524=CARTESIAN_POINT ( 'NONE',  ( 4.000000000000000000, 0.000000000000000000, 22.00000000000000355 ) ) ;
#6531=EDGE_CURVE ( 'NONE', #7382, #5267, #3348, .T. ) ;
#6535=DIRECTION ( 'NONE',  ( -1.000000000000000000, -0.000000000000000000, -0.000000000000000000 ) ) ;
#6537=ORIENTED_EDGE ( 'NONE', *, *, #2885, .T. ) ;
#6542=LINE ( 'NONE', #7394, #2578 ) ;
#6545=EDGE_CURVE ( 'NONE', #6084, #3451, #5039, .T. ) ;
#6549=DIRECTION ( 'NONE',  ( 0.000000000000000000, 0.000000000000000000, 1.000000000000000000 ) ) ;
#6559=AXIS2_PLACEMENT_3D ( 'NONE', #113, #6752, #8896 ) ;
#6561=AXIS2_PLACEMENT_3D ( 'NONE', #3462, #9271, #6459 ) ;
#6569=DIRECTION ( 'NONE',  ( -1.000000000000000000, 0.000000000000000000, 0.000000000000000000 ) ) ;
#6572=VECTOR ( 'NONE', #1962, 1000.000000000000000 ) ;
#6575=CARTESIAN_POINT ( 'NONE',  ( 19.00000000000000000, 0.000000000000000000, 0.000000000000000000 ) ) ;
#6577=EDGE_LOOP ( 'NONE', ( #8915, #7552 ) ) ;
#6583=AXIS2_PLACEMENT_3D ( 'NONE', #2222, #5106, #1653 ) ;
#6589=EDGE_LOOP ( 'NONE', ( #8970, #4328, #2644, #9114 ) ) ;
#6595=EDGE_CURVE ( 'NONE', #3451, #2056, #9245, .T. ) ;
#6600=DIRECTION ( 'NONE',  ( 0.000000000000000000, 0.000000000000000000, -1.000000000000000000 ) ) ;
#6604=DIRECTION ( 'NONE',  ( -1.000000000000000000, -0.000000000000000000, -0.000000000000000000 ) ) ;
#6614=CARTESIAN_POINT ( 'NONE',  ( 0.4999999999999935052, 0.000000000000000000, 0.000000000000000000 ) ) ;
#6615=DIRECTION ( 'NONE',  ( 0.000000000000000000, 0.000000000000000000, -1.000000000000000000 ) ) ;
#6617=DIRECTION ( 'NONE',  ( 1.000000000000000000, 0.000000000000000000, 0.000000000000000000 ) ) ;
#6621=CYLINDRICAL_SURFACE ( 'NONE', #669, 13.66147716702868031 ) ;
#6622=EDGE_LOOP ( 'NONE', ( #4985, #4485 ) ) ;
#6628=CYLINDRICAL_SURFACE ( 'NONE', #70, 1.560000000002327303 ) ;
#6644=ORIENTED_EDGE ( 'NONE', *, *, #9124, .T. ) ;
#6648=DIRECTION ( 'NONE',  ( 0.000000000000000000, 0.000000000000000000, -1.000000000000000000 ) ) ;
#6676=CARTESIAN_POINT ( 'NONE',  ( 4.000000000000000000, -9.628187502531647418E-13, -18.43999999999823913 ) ) ;
#6684=CARTESIAN_POINT ( 'NONE',  ( 0.000000000000000000, 0.000000000000000000, 0.000000000000000000 ) ) ;
#6686=CARTESIAN_POINT ( 'NONE',  ( 5.000000000000000000, -9.628187502531647418E-13, -19.99999999999950262 ) ) ;
#6694=CYLINDRICAL_SURFACE ( 'NONE', #6559, 17.50000000000000000 ) ;
#6697=AXIS2_PLACEMENT_3D ( 'NONE', #2388, #6617, #6707 ) ;
#6698=ORIENTED_EDGE ( 'NONE', *, *, #1393, .F. ) ;
#6699=PRODUCT ( '2-Bush', '2-Bush', '', ( #294 ) ) ;
#6707=DIRECTION ( 'NONE',  ( 0.000000000000000000, 0.000000000000000000, -1.000000000000000000 ) ) ;
#6713=CARTESIAN_POINT ( 'NONE',  ( 0.000000000000000000, 1.917977788252103204E-15, -15.66147716702868209 ) ) ;
#6737=EDGE_CURVE ( 'NONE', #1115, #1485, #9176, .T. ) ;
#6740=AXIS2_PLACEMENT_3D ( 'NONE', #2484, #7516, #268 ) ;
#6742=CARTESIAN_POINT ( 'NONE',  ( 5.000000000000000000, -14.14213562373112154, 14.14213562373418220 ) ) ;
#6744=LINE ( 'NONE', #7446, #4594 ) ;
#6748=ORIENTED_EDGE ( 'NONE', *, *, #1905, .T. ) ;
#6750=ORIENTED_EDGE ( 'NONE', *, *, #5865, .T. ) ;
#6752=DIRECTION ( 'NONE',  ( -1.000000000000000000, -0.000000000000000000, -0.000000000000000000 ) ) ;
#6753=DIRECTION ( 'NONE',  ( 0.000000000000000000, 0.000000000000000000, -1.000000000000000000 ) ) ;
#6760=CARTESIAN_POINT ( 'NONE',  ( 0.000000000000000000, 0.000000000000000000, 0.000000000000000000 ) ) ;
#6761=ORIENTED_EDGE ( 'NONE', *, *, #6777, .F. ) ;
#6775=DIRECTION ( 'NONE',  ( -1.000000000000000000, 0.000000000000000000, 0.000000000000000000 ) ) ;
#6777=EDGE_CURVE ( 'NONE', #6239, #1041, #7961, .T. ) ;
#6778=DIRECTION ( 'NONE',  ( -1.000000000000000000, -0.000000000000000000, -0.000000000000000000 ) ) ;
#6781=ORIENTED_EDGE ( 'NONE', *, *, #3599, .T. ) ;
#6784=VECTOR ( 'NONE', #3324, 1000.000000000000000 ) ;
#6795=VECTOR ( 'NONE', #5686, 1000.000000000000000 ) ;
#6800=ORIENTED_EDGE ( 'NONE', *, *, #1525, .F. ) ;
#6828=DIRECTION ( 'NONE',  ( 0.000000000000000000, 0.000000000000000000, 1.000000000000000000 ) ) ;
#6842=CARTESIAN_POINT ( 'NONE',  ( 4.000000000000000000, 7.653668647302530381, 19.22759065022631830 ) ) ;
#6843=EDGE_CURVE ( 'NONE', #3983, #2056, #1971, .T. ) ;
#6845=CARTESIAN_POINT ( 'NONE',  ( 5.000000000000000000, 20.00000000000120437, 1.559999999999680531 ) ) ;
#6848=ORIENTED_EDGE ( 'NONE', *, *, #6246, .F. ) ;
#6851=EDGE_LOOP ( 'NONE', ( #1114, #6302, #4089, #4848 ) ) ;
#6856=CARTESIAN_POINT ( 'NONE',  ( 0.4999999999999935052, 0.000000000000000000, 0.000000000000000000 ) ) ;
#6875=ORIENTED_EDGE ( 'NONE', *, *, #5945, .T. ) ;
#6887=ORIENTED_EDGE ( 'NONE', *, *, #7826, .F. ) ;
#6899=EDGE_LOOP ( 'NONE', ( #9315, #8110, #6875, #7 ) ) ;
#6902=ORIENTED_EDGE ( 'NONE', *, *, #4168, .F. ) ;
#6905=CARTESIAN_POINT ( 'NONE',  ( 0.000000000000000000, -14.14213562373248401, -14.14213562372942157 ) ) ;
#6906=DIRECTION ( 'NONE',  ( 1.000000000000000000, 0.000000000000000000, 0.000000000000000000 ) ) ;
#6912=VERTEX_POINT ( 'NONE', #3971 ) ;
#6938=AXIS2_PLACEMENT_3D ( 'NONE', #5145, #8839, #3081 ) ;
#6958=CARTESIAN_POINT ( 'NONE',  ( 4.000000000000000000, 18.47759065022580316, -6.903668647301629768 ) ) ;
#6959=EDGE_LOOP ( 'NONE', ( #8315, #3135, #2524, #5785 ) ) ;
#6985=DIRECTION ( 'NONE',  ( 0.000000000000000000, 0.000000000000000000, 1.000000000000000000 ) ) ;
#6988=ORIENTED_EDGE ( 'NONE', *, *, #889, .F. ) ;
#6997=CARTESIAN_POINT ( 'NONE',  ( 4.000000000000000000, -18.47759065022712832, 7.653668647304757044 ) ) ;
#7006=DIRECTION ( 'NONE',  ( 0.000000000000000000, 0.000000000000000000, -1.000000000000000000 ) ) ;
#7011=VECTOR ( 'NONE', #8672, 1000.000000000000000 ) ;
#7014=ADVANCED_FACE ( 'NONE', ( #1941, #5554, #1894, #4962, #5743, #1990, #7121, #542, #1165, #2035, #5600, #4105, #4821, #494, #3468, #1305, #9232, #9379 ), #6413, .T. ) ;
#7016=AXIS2_PLACEMENT_3D ( 'NONE', #6174, #3138, #9041 ) ;
#7019=VECTOR ( 'NONE', #478, 1000.000000000000114 ) ;
#7026=AXIS2_PLACEMENT_3D ( 'NONE', #8877, #6775, #1679 ) ;
#7029=DIRECTION ( 'NONE',  ( -1.000000000000000000, -0.000000000000000000, -0.000000000000000000 ) ) ;
#7030=LINE ( 'NONE', #6845, #6784 ) ;
#7035=EDGE_LOOP ( 'NONE', ( #6425, #8327 ) ) ;
#7039=DIRECTION ( 'NONE',  ( -1.000000000000000000, 0.000000000000000000, 0.000000000000000000 ) ) ;
#7052=DIRECTION ( 'NONE',  ( -1.000000000000000000, -0.000000000000000000, -0.000000000000000000 ) ) ;
#7060=EDGE_CURVE ( 'NONE', #8187, #8436, #8785, .T. ) ;
#7069=ORIENTED_EDGE ( 'NONE', *, *, #7402, .T. ) ;
#7072=CYLINDRICAL_SURFACE ( 'NONE', #8892, 0.7500000000013684609 ) ;
#7076=ORIENTED_EDGE ( 'NONE', *, *, #7109, .F. ) ;
#7079=CARTESIAN_POINT ( 'NONE',  ( 2.000000000000000000, 0.000000000000000000, 0.000000000000000000 ) ) ;
#7080=CARTESIAN_POINT ( 'NONE',  ( 4.000000000000000000, 18.47759065022658120, 7.653668647302884764 ) ) ;
#7082=CARTESIAN_POINT ( 'NONE',  ( 4.000000000000000000, 14.14213562373112154, -14.14213562373077870 ) ) ;
#7096=ORIENTED_EDGE ( 'NONE', *, *, #8640, .F. ) ;
#7103=EDGE_LOOP ( 'NONE', ( #3282, #1999 ) ) ;
#7104=ORIENTED_EDGE ( 'NONE', *, *, #2739, .F. ) ;
#7109=EDGE_CURVE ( 'NONE', #2056, #4903, #6035, .T. ) ;
#7115=FACE_BOUND ( 'NONE', #6320, .T. ) ;
#7121=FACE_BOUND ( 'NONE', #1200, .T. ) ;
#7131=ORIENTED_EDGE ( 'NONE', *, *, #1850, .F. ) ;
#7134=CARTESIAN_POINT ( 'NONE',  ( 4.000000000000000000, -9.628187502531647418E-13, -19.99999999999950262 ) ) ;
#7136=CARTESIAN_POINT ( 'NONE',  ( 19.00000000000000000, 0.000000000000000000, 0.000000000000000000 ) ) ;
#7139=DIRECTION ( 'NONE',  ( 1.000000000000000000, 0.000000000000000000, 0.000000000000000000 ) ) ;
#7151=CARTESIAN_POINT ( 'NONE',  ( 3.499999999999999556, 2.755455298081544778E-15, -22.50000000000000000 ) ) ;
#7157=AXIS2_PLACEMENT_3D ( 'NONE', #7757, #7039, #779 ) ;
#7161=CIRCLE ( 'NONE', #3331, 1.560000000001265263 ) ;
#7169=EDGE_LOOP ( 'NONE', ( #1559, #8742, #363, #6059 ) ) ;
#7170=DIRECTION ( 'NONE',  ( -1.000000000000000000, 0.000000000000000000, 0.000000000000000000 ) ) ;
#7174=EDGE_CURVE ( 'NONE', #5769, #6494, #8628, .T. ) ;
#7180=CARTESIAN_POINT ( 'NONE',  ( 4.000000000000000000, 14.14213562373112154, -12.58213562373077821 ) ) ;
#7186=LINE ( 'NONE', #4353, #3166 ) ;
#7190=DIRECTION ( 'NONE',  ( -1.000000000000000000, -0.000000000000000000, -0.000000000000000000 ) ) ;
#7194=CARTESIAN_POINT ( 'NONE',  ( 5.000000000000000000, 14.14213562373247868, 14.14213562373282329 ) ) ;
#7200=ORIENTED_EDGE ( 'NONE', *, *, #8251, .T. ) ;
#7202=ORIENTED_EDGE ( 'NONE', *, *, #7706, .T. ) ;
#7208=ADVANCED_FACE ( 'NONE', ( #2899 ), #4180, .T. ) ;
#7211=CARTESIAN_POINT ( 'NONE',  ( 0.000000000000000000, 0.000000000000000000, 0.000000000000000000 ) ) ;
#7222=EDGE_LOOP ( 'NONE', ( #45, #8434 ) ) ;
#7235=DIRECTION ( 'NONE',  ( 0.000000000000000000, 0.000000000000000000, 1.000000000000000000 ) ) ;
#7236=ORIENTED_EDGE ( 'NONE', *, *, #1912, .F. ) ;
#7239=DIRECTION ( 'NONE',  ( -1.000000000000000000, -0.000000000000000000, -0.000000000000000000 ) ) ;
#7241=ADVANCED_FACE ( 'NONE', ( #4384 ), #736, .T. ) ;
#7251=VERTEX_POINT ( 'NONE', #6125 ) ;
#7257=CARTESIAN_POINT ( 'NONE',  ( 19.00000000000000000, 0.000000000000000000, 13.66147716702868031 ) ) ;
#7263=DIRECTION ( 'NONE',  ( 1.000000000000000000, 0.000000000000000000, 0.000000000000000000 ) ) ;
#7269=ORIENTED_EDGE ( 'NONE', *, *, #847, .T. ) ;
#7287=( GEOMETRIC_REPRESENTATION_CONTEXT ( 3 ) GLOBAL_UNCERTAINTY_ASSIGNED_CONTEXT ( ( #92 ) ) GLOBAL_UNIT_ASSIGNED_CONTEXT ( ( #7663, #8379, #3096 ) ) REPRESENTATION_CONTEXT ( 'NONE', 'WORKASPACE' ) );
#7305=FACE_BOUND ( 'NONE', #2972, .T. ) ;
#7311=DIRECTION ( 'NONE',  ( 0.000000000000000000, 0.000000000000000000, -1.000000000000000000 ) ) ;
#7329=DIRECTION ( 'NONE',  ( 0.000000000000000000, 0.000000000000000000, 1.000000000000000000 ) ) ;
#7350=DIRECTION ( 'NONE',  ( -1.000000000000000000, -0.000000000000000000, -0.000000000000000000 ) ) ;
#7353=DIRECTION ( 'NONE',  ( 1.000000000000000000, 0.000000000000000000, 0.000000000000000000 ) ) ;
#7356=ORIENTED_EDGE ( 'NONE', *, *, #9403, .T. ) ;
#7369=ORIENTED_EDGE ( 'NONE', *, *, #5924, .T. ) ;
#7375=DIRECTION ( 'NONE',  ( -1.000000000000000000, -0.000000000000000000, -0.000000000000000000 ) ) ;
#7378=ORIENTED_EDGE ( 'NONE', *, *, #5666, .T. ) ;
#7382=VERTEX_POINT ( 'NONE', #8370 ) ;
#7394=CARTESIAN_POINT ( 'NONE',  ( 5.000000000000000000, 18.47759065022658120, 8.403668647301545391 ) ) ;
#7398=FACE_OUTER_BOUND ( 'NONE', #7787, .T. ) ;
#7402=EDGE_CURVE ( 'NONE', #8405, #2113, #3722, .T. ) ;
#7403=EDGE_CURVE ( 'NONE', #602, #3367, #8467, .T. ) ;
#7405=VERTEX_POINT ( 'NONE', #5635 ) ;
#7412=EDGE_LOOP ( 'NONE', ( #904, #66, #5837, #1858 ) ) ;
#7433=VECTOR ( 'NONE', #8461, 1000.000000000000114 ) ;
#7436=VERTEX_POINT ( 'NONE', #3369 ) ;
#7446=CARTESIAN_POINT ( 'NONE',  ( 0.000000000000000000, 0.000000000000000000, 22.50000000000000000 ) ) ;
#7453=FACE_OUTER_BOUND ( 'NONE', #827, .T. ) ;
#7468=CIRCLE ( 'NONE', #4863, 2.000000000000000000 ) ;
#7474=CARTESIAN_POINT ( 'NONE',  ( 5.000000000000000000, 20.00000000000120437, -1.559999999998198161 ) ) ;
#7483=CIRCLE ( 'NONE', #887, 1.560000000000134168 ) ;
#7489=ORIENTED_EDGE ( 'NONE', *, *, #4066, .F. ) ;
#7495=PRODUCT_DEFINITION_CONTEXT ( 'detailed design', #996, 'design' ) ;
#7498=CYLINDRICAL_SURFACE ( 'NONE', #6938, 0.7499999999986606269 ) ;
#7499=LINE ( 'NONE', #2607, #5816 ) ;
#7509=DIRECTION ( 'NONE',  ( -1.000000000000000000, -0.000000000000000000, -0.000000000000000000 ) ) ;
#7516=DIRECTION ( 'NONE',  ( -1.000000000000000000, 0.000000000000000000, 0.000000000000000000 ) ) ;
#7525=EDGE_CURVE ( 'NONE', #4838, #943, #5413, .T. ) ;
#7537=AXIS2_PLACEMENT_3D ( 'NONE', #5651, #8525, #1309 ) ;
#7541=VERTEX_POINT ( 'NONE', #390 ) ;
#7544=CYLINDRICAL_SURFACE ( 'NONE', #2858, 0.7500000000012114754 ) ;
#7547=FACE_OUTER_BOUND ( 'NONE', #8904, .T. ) ;
#7548=DIRECTION ( 'NONE',  ( 0.000000000000000000, 0.000000000000000000, 1.000000000000000000 ) ) ;
#7552=ORIENTED_EDGE ( 'NONE', *, *, #6131, .T. ) ;
#7554=DIRECTION ( 'NONE',  ( -1.000000000000000000, 0.000000000000000000, 0.000000000000000000 ) ) ;
#7572=ORIENTED_EDGE ( 'NONE', *, *, #8529, .F. ) ;
#7574=CARTESIAN_POINT ( 'NONE',  ( 19.00000000000000000, 0.000000000000000000, 0.000000000000000000 ) ) ;
#7586=CIRCLE ( 'NONE', #8045, 15.66147716702868209 ) ;
#7587=CARTESIAN_POINT ( 'NONE',  ( 5.000000000000000000, 7.653668647300657213, -18.47759065022568237 ) ) ;
#7601=FACE_OUTER_BOUND ( 'NONE', #6899, .T. ) ;
#7602=CYLINDRICAL_SURFACE ( 'NONE', #189, 1.560000000000000719 ) ;
#7622=AXIS2_PLACEMENT_3D ( 'NONE', #1650, #8371, #348 ) ;
#7625=ORIENTED_EDGE ( 'NONE', *, *, #1833, .T. ) ;
#7632=CIRCLE ( 'NONE', #1648, 1.560000000002236709 ) ;
#7637=AXIS2_PLACEMENT_3D ( 'NONE', #142, #5853, #3066 ) ;
#7644=DIRECTION ( 'NONE',  ( -1.000000000000000000, -0.000000000000000000, -0.000000000000000000 ) ) ;
#7647=ORIENTED_EDGE ( 'NONE', *, *, #7908, .F. ) ;
#7662=ORIENTED_EDGE ( 'NONE', *, *, #8071, .T. ) ;
#7663=( LENGTH_UNIT ( ) NAMED_UNIT ( * ) SI_UNIT ( .MILLI., .METRE. ) );
#7664=ORIENTED_EDGE ( 'NONE', *, *, #8177, .F. ) ;
#7683=CIRCLE ( 'NONE', #323, 0.7499999999982936982 ) ;
#7688=ADVANCED_FACE ( 'NONE', ( #245 ), #7544, .F. ) ;
#7689=VECTOR ( 'NONE', #6418, 1000.000000000000000 ) ;
#7696=CYLINDRICAL_SURFACE ( 'NONE', #1333, 1.559999999999096776 ) ;
#7706=EDGE_CURVE ( 'NONE', #1656, #4910, #4085, .T. ) ;
#7725=DIRECTION ( 'NONE',  ( 0.000000000000000000, 0.000000000000000000, 1.000000000000000000 ) ) ;
#7743=CIRCLE ( 'NONE', #9421, 0.7499999999986606269 ) ;
#7757=CARTESIAN_POINT ( 'NONE',  ( 0.000000000000000000, -18.47759065022790637, -7.653668647299759265 ) ) ;
#7758=CARTESIAN_POINT ( 'NONE',  ( 4.000000000000000000, 18.47759065022658120, 8.403668647301545391 ) ) ;
#7776=CIRCLE ( 'NONE', #1944, 0.7499999999986606269 ) ;
#7779=ORIENTED_EDGE ( 'NONE', *, *, #847, .F. ) ;
#7787=EDGE_LOOP ( 'NONE', ( #3388, #6295, #4227, #2679 ) ) ;
#7788=( GEOMETRIC_REPRESENTATION_CONTEXT ( 3 ) GLOBAL_UNCERTAINTY_ASSIGNED_CONTEXT ( ( #4419 ) ) GLOBAL_UNIT_ASSIGNED_CONTEXT ( ( #1594, #210, #4674 ) ) REPRESENTATION_CONTEXT ( 'NONE', 'WORKASPACE' ) );
#7797=CYLINDRICAL_SURFACE ( 'NONE', #679, 0.7500000000001915135 ) ;
#7803=DIRECTION ( 'NONE',  ( 0.000000000000000000, 0.000000000000000000, 1.000000000000000000 ) ) ;
#7826=EDGE_CURVE ( 'NONE', #1835, #5764, #6243, .T. ) ;
#7832=ORIENTED_EDGE ( 'NONE', *, *, #6595, .T. ) ;
#7835=VECTOR ( 'NONE', #7863, 1000.000000000000000 ) ;
#7837=EDGE_CURVE ( 'NONE', #5476, #5740, #2709, .T. ) ;
#7844=FACE_BOUND ( 'NONE', #2656, .T. ) ;
#7853=CIRCLE ( 'NONE', #782, 1.560000000000002274 ) ;
#7855=VERTEX_POINT ( 'NONE', #7964 ) ;
#7859=EDGE_CURVE ( 'NONE', #1986, #1900, #2777, .T. ) ;
#7863=DIRECTION ( 'NONE',  ( -1.000000000000000000, -0.000000000000000000, -0.000000000000000000 ) ) ;
#7867=FACE_OUTER_BOUND ( 'NONE', #2504, .T. ) ;
#7869=ORIENTED_EDGE ( 'NONE', *, *, #1178, .T. ) ;
#7870=FACE_OUTER_BOUND ( 'NONE', #9066, .T. ) ;
#7876=CARTESIAN_POINT ( 'NONE',  ( 0.000000000000000000, -9.628187502531647418E-13, -19.99999999999950262 ) ) ;
#7878=EDGE_LOOP ( 'NONE', ( #1244, #7664 ) ) ;
#7886=FACE_OUTER_BOUND ( 'NONE', #6095, .T. ) ;
#7888=CARTESIAN_POINT ( 'NONE',  ( 4.000000000000000000, 0.000000000000000000, 0.000000000000000000 ) ) ;
#7890=DIRECTION ( 'NONE',  ( -1.000000000000000000, -0.000000000000000000, -0.000000000000000000 ) ) ;
#7891=CIRCLE ( 'NONE', #3749, 22.50000000000000000 ) ;
#7892=ORIENTED_EDGE ( 'NONE', *, *, #9124, .F. ) ;
#7897=LINE ( 'NONE', #498, #9115 ) ;
#7908=EDGE_CURVE ( 'NONE', #5068, #2924, #7186, .T. ) ;
#7915=FACE_OUTER_BOUND ( 'NONE', #5209, .T. ) ;
#7924=EDGE_CURVE ( 'NONE', #3451, #6084, #4702, .T. ) ;
#7927=CIRCLE ( 'NONE', #6406, 1.559999999998939346 ) ;
#7943=EDGE_CURVE ( 'NONE', #1986, #4149, #3941, .T. ) ;
#7945=AXIS2_PLACEMENT_3D ( 'NONE', #1568, #5803, #8732 ) ;
#7957=ORIENTED_EDGE ( 'NONE', *, *, #1008, .F. ) ;
#7961=CIRCLE ( 'NONE', #3495, 1.560000000002327303 ) ;
#7964=CARTESIAN_POINT ( 'NONE',  ( 0.000000000000000000, -18.47759065022790637, -8.403668647301127947 ) ) ;
#7967=DIRECTION ( 'NONE',  ( 0.000000000000000000, 0.000000000000000000, 1.000000000000000000 ) ) ;
#7971=DIRECTION ( 'NONE',  ( 0.000000000000000000, 0.000000000000000000, -1.000000000000000000 ) ) ;
#7975=DIRECTION ( 'NONE',  ( -1.000000000000000000, -0.000000000000000000, -0.000000000000000000 ) ) ;
#7977=ORIENTED_EDGE ( 'NONE', *, *, #3257, .F. ) ;
#7984=FACE_OUTER_BOUND ( 'NONE', #4250, .T. ) ;
#7987=DIRECTION ( 'NONE',  ( 0.000000000000000000, 0.000000000000000000, 1.000000000000000000 ) ) ;
#7990=CARTESIAN_POINT ( 'NONE',  ( 5.000000000000000000, 20.00000000000120437, 7.412591687719288072E-13 ) ) ;
#7991=CIRCLE ( 'NONE', #627, 22.50000000000000000 ) ;
#8027=CARTESIAN_POINT ( 'NONE',  ( 0.000000000000000000, 20.00000000000120437, -1.559999999998198161 ) ) ;
#8028=LINE ( 'NONE', #5971, #5370 ) ;
#8035=EDGE_CURVE ( 'NONE', #4149, #1986, #8230, .T. ) ;
#8038=CARTESIAN_POINT ( 'NONE',  ( 4.000000000000000000, 7.653668647302530381, 17.72759065022973246 ) ) ;
#8043=ORIENTED_EDGE ( 'NONE', *, *, #7943, .T. ) ;
#8044=DIRECTION ( 'NONE',  ( 0.000000000000000000, 0.000000000000000000, 1.000000000000000000 ) ) ;
#8045=AXIS2_PLACEMENT_3D ( 'NONE', #3062, #133, #7967 ) ;
#8049=CARTESIAN_POINT ( 'NONE',  ( 0.000000000000000000, 18.47759065022580316, -7.653668647301631545 ) ) ;
#8054=CARTESIAN_POINT ( 'NONE',  ( 5.000000000000000000, 14.14213562373112154, -12.58213562373077821 ) ) ;
#8062=EDGE_CURVE ( 'NONE', #2916, #4498, #3780, .T. ) ;
#8068=ORIENTED_EDGE ( 'NONE', *, *, #5673, .F. ) ;
#8069=VERTEX_POINT ( 'NONE', #5115 ) ;
#8070=VERTEX_POINT ( 'NONE', #4543 ) ;
#8071=EDGE_CURVE ( 'NONE', #3554, #2947, #747, .T. ) ;
#8085=ORIENTED_EDGE ( 'NONE', *, *, #1072, .T. ) ;
#8086=DIRECTION ( 'NONE',  ( 1.000000000000000000, 0.000000000000000000, 0.000000000000000000 ) ) ;
#8092=CARTESIAN_POINT ( 'NONE',  ( 0.000000000000000000, 2.724839128102860991E-15, 22.00000000000000711 ) ) ;
#8108=DIRECTION ( 'NONE',  ( 0.000000000000000000, 0.000000000000000000, -1.000000000000000000 ) ) ;
#8109=ORIENTED_EDGE ( 'NONE', *, *, #8640, .T. ) ;
#8110=ORIENTED_EDGE ( 'NONE', *, *, #8618, .T. ) ;
#8117=CIRCLE ( 'NONE', #9028, 0.7499999999982936982 ) ;
#8118=EDGE_CURVE ( 'NONE', #4695, #3685, #5634, .T. ) ;
#8123=CARTESIAN_POINT ( 'NONE',  ( 4.000000000000000000, -20.00000000000120437, 2.661998082081668380E-12 ) ) ;
#8130=DIRECTION ( 'NONE',  ( 0.000000000000000000, 0.000000000000000000, -1.000000000000000000 ) ) ;
#8153=LINE ( 'NONE', #1567, #2378 ) ;
#8156=ORIENTED_EDGE ( 'NONE', *, *, #8614, .F. ) ;
#8159=ORIENTED_EDGE ( 'NONE', *, *, #1178, .F. ) ;
#8177=EDGE_CURVE ( 'NONE', #5087, #9340, #9296, .T. ) ;
#8187=VERTEX_POINT ( 'NONE', #4783 ) ;
#8191=CARTESIAN_POINT ( 'NONE',  ( 4.000000000000000000, -18.47759065022790637, -8.403668647301127947 ) ) ;
#8194=DIRECTION ( 'NONE',  ( 0.000000000000000000, 0.000000000000000000, -1.000000000000000000 ) ) ;
#8214=CARTESIAN_POINT ( 'NONE',  ( 0.000000000000000000, -20.00000000000120437, 2.661998082081668380E-12 ) ) ;
#8216=DIRECTION ( 'NONE',  ( -1.000000000000000000, -0.000000000000000000, -0.000000000000000000 ) ) ;
#8219=DIRECTION ( 'NONE',  ( -1.000000000000000000, -0.000000000000000000, -0.000000000000000000 ) ) ;
#8227=CARTESIAN_POINT ( 'NONE',  ( 5.000000000000000000, 9.603694566548697359E-13, 20.00000000000290612 ) ) ;
#8230=CIRCLE ( 'NONE', #6697, 0.7500000000012114754 ) ;
#8243=EDGE_CURVE ( 'NONE', #23, #8998, #8837, .T. ) ;
#8244=DIRECTION ( 'NONE',  ( -1.000000000000000000, 0.000000000000000000, 0.000000000000000000 ) ) ;
#8245=AXIS2_PLACEMENT_3D ( 'NONE', #1985, #4909, #9323 ) ;
#8251=EDGE_CURVE ( 'NONE', #424, #4140, #7776, .T. ) ;
#8264=CARTESIAN_POINT ( 'NONE',  ( 0.000000000000000000, -20.00000000000120437, 1.560000000004989174 ) ) ;
#8302=DIRECTION ( 'NONE',  ( -1.000000000000000000, -0.000000000000000000, -0.000000000000000000 ) ) ;
#8310=DIRECTION ( 'NONE',  ( -1.000000000000000000, -0.000000000000000000, -0.000000000000000000 ) ) ;
#8311=CIRCLE ( 'NONE', #9075, 1.560000000002327303 ) ;
#8313=CARTESIAN_POINT ( 'NONE',  ( 5.000000000000000000, -18.47759065022712832, 7.653668647304757044 ) ) ;
#8315=ORIENTED_EDGE ( 'NONE', *, *, #5242, .F. ) ;
#8327=ORIENTED_EDGE ( 'NONE', *, *, #8618, .F. ) ;
#8328=AXIS2_PLACEMENT_3D ( 'NONE', #4152, #2623, #6464 ) ;
#8335=VECTOR ( 'NONE', #3270, 1000.000000000000000 ) ;
#8339=DIRECTION ( 'NONE',  ( 1.000000000000000000, 0.000000000000000000, 0.000000000000000000 ) ) ;
#8344=CARTESIAN_POINT ( 'NONE',  ( 4.000000000000000000, -18.47759065022790637, -7.653668647299759265 ) ) ;
#8345=ADVANCED_FACE ( 'NONE', ( #2806 ), #5745, .T. ) ;
#8347=ADVANCED_FACE ( 'NONE', ( #4107 ), #9428, .F. ) ;
#8351=CIRCLE ( 'NONE', #377, 1.560000000002236709 ) ;
#8353=EDGE_CURVE ( 'NONE', #4159, #7855, #9004, .T. ) ;
#8357=ADVANCED_FACE ( 'NONE', ( #2221 ), #5878, .F. ) ;
#8366=EDGE_LOOP ( 'NONE', ( #7096, #4025 ) ) ;
#8368=ORIENTED_EDGE ( 'NONE', *, *, #3015, .F. ) ;
#8370=CARTESIAN_POINT ( 'NONE',  ( 4.000000000000000000, -18.47759065022712832, 8.403668647304948891 ) ) ;
#8371=DIRECTION ( 'NONE',  ( 1.000000000000000000, 0.000000000000000000, 0.000000000000000000 ) ) ;
#8379=( NAMED_UNIT ( * ) PLANE_ANGLE_UNIT ( ) SI_UNIT ( $, .RADIAN. ) );
#8382=DIRECTION ( 'NONE',  ( 0.000000000000000000, -1.224646799147353454E-16, 1.000000000000000000 ) ) ;
#8391=DIRECTION ( 'NONE',  ( -1.000000000000000000, -0.000000000000000000, -0.000000000000000000 ) ) ;
#8392=ORIENTED_EDGE ( 'NONE', *, *, #4456, .F. ) ;
#8401=LINE ( 'NONE', #5335, #2831 ) ;
#8405=VERTEX_POINT ( 'NONE', #168 ) ;
#8406=CIRCLE ( 'NONE', #7945, 1.560000000001265263 ) ;
#8408=CONICAL_SURFACE ( 'NONE', #126, 22.00000000000000711, 0.7853981633974482790 ) ;
#8422=AXIS2_PLACEMENT_3D ( 'NONE', #6614, #4306, #8044 ) ;
#8426=EDGE_CURVE ( 'NONE', #85, #4903, #7468, .T. ) ;
#8434=ORIENTED_EDGE ( 'NONE', *, *, #6465, .F. ) ;
#8436=VERTEX_POINT ( 'NONE', #1502 ) ;
#8437=DIRECTION ( 'NONE',  ( -0.000000000000000000, 1.000000000000000000, 1.224646799147353207E-16 ) ) ;
#8443=EDGE_LOOP ( 'NONE', ( #2351, #8834, #6902, #2666 ) ) ;
#8449=ORIENTED_EDGE ( 'NONE', *, *, #5010, .F. ) ;
#8460=CARTESIAN_POINT ( 'NONE',  ( 0.000000000000000000, 0.000000000000000000, 0.000000000000000000 ) ) ;
#8461=DIRECTION ( 'NONE',  ( -0.7071067811865500152, 0.000000000000000000, 0.7071067811865451302 ) ) ;
#8467=LINE ( 'NONE', #1291, #6795 ) ;
#8471=ADVANCED_FACE ( 'NONE', ( #5105 ), #6694, .T. ) ;
#8472=DIRECTION ( 'NONE',  ( -1.000000000000000000, -0.000000000000000000, -0.000000000000000000 ) ) ;
#8473=ADVANCED_FACE ( 'NONE', ( #7453 ), #875, .F. ) ;
#8475=VECTOR ( 'NONE', #2212, 1000.000000000000000 ) ;
#8481=AXIS2_PLACEMENT_3D ( 'NONE', #3411, #4809, #6402 ) ;
#8488=ORIENTED_EDGE ( 'NONE', *, *, #8757, .T. ) ;
#8490=ORIENTED_EDGE ( 'NONE', *, *, #8071, .F. ) ;
#8493=ORIENTED_EDGE ( 'NONE', *, *, #6545, .F. ) ;
#8494=DIRECTION ( 'NONE',  ( 0.000000000000000000, 0.000000000000000000, 1.000000000000000000 ) ) ;
#8500=AXIS2_PLACEMENT_3D ( 'NONE', #2490, #278, #182 ) ;
#8504=DIRECTION ( 'NONE',  ( -1.000000000000000000, -0.000000000000000000, -0.000000000000000000 ) ) ;
#8506=ORIENTED_EDGE ( 'NONE', *, *, #6043, .F. ) ;
#8523=DIRECTION ( 'NONE',  ( 0.000000000000000000, 0.000000000000000000, -1.000000000000000000 ) ) ;
#8525=DIRECTION ( 'NONE',  ( -1.000000000000000000, -0.000000000000000000, -0.000000000000000000 ) ) ;
#8526=ADVANCED_FACE ( 'NONE', ( #4583 ), #5496, .F. ) ;
#8528=ADVANCED_FACE ( 'NONE', ( #391 ), #8990, .F. ) ;
#8529=EDGE_CURVE ( 'NONE', #3983, #85, #3637, .T. ) ;
#8533=ORIENTED_EDGE ( 'NONE', *, *, #6304, .F. ) ;
#8551=DIRECTION ( 'NONE',  ( 0.000000000000000000, 0.000000000000000000, 1.000000000000000000 ) ) ;
#8573=CIRCLE ( 'NONE', #8422, 22.50000000000000000 ) ;
#8583=DIRECTION ( 'NONE',  ( 0.000000000000000000, 0.000000000000000000, 1.000000000000000000 ) ) ;
#8587=LINE ( 'NONE', #2781, #3959 ) ;
#8589=ORIENTED_EDGE ( 'NONE', *, *, #8251, .F. ) ;
#8598=ORIENTED_EDGE ( 'NONE', *, *, #4943, .T. ) ;
#8610=VERTEX_POINT ( 'NONE', #6842 ) ;
#8614=EDGE_CURVE ( 'NONE', #1485, #1115, #4712, .T. ) ;
#8618=EDGE_CURVE ( 'NONE', #8070, #3385, #7927, .T. ) ;
#8621=EDGE_LOOP ( 'NONE', ( #8533, #2585 ) ) ;
#8623=ORIENTED_EDGE ( 'NONE', *, *, #7060, .F. ) ;
#8628=CIRCLE ( 'NONE', #4645, 0.7500000000000006661 ) ;
#8633=ORIENTED_EDGE ( 'NONE', *, *, #3953, .T. ) ;
#8640=EDGE_CURVE ( 'NONE', #2987, #9037, #2248, .T. ) ;
#8645=EDGE_LOOP ( 'NONE', ( #1569, #8633, #3316, #969 ) ) ;
#8655=CYLINDRICAL_SURFACE ( 'NONE', #6327, 1.560000000002236709 ) ;
#8656=CIRCLE ( 'NONE', #825, 0.7499999999982936982 ) ;
#8671=ORIENTED_EDGE ( 'NONE', *, *, #1735, .T. ) ;
#8672=DIRECTION ( 'NONE',  ( -1.000000000000000000, -0.000000000000000000, -0.000000000000000000 ) ) ;
#8675=DIRECTION ( 'NONE',  ( -1.000000000000000000, -0.000000000000000000, -0.000000000000000000 ) ) ;
#8677=DIRECTION ( 'NONE',  ( -1.000000000000000000, -0.000000000000000000, -0.000000000000000000 ) ) ;
#8684=CARTESIAN_POINT ( 'NONE',  ( 4.000000000000000000, -7.653668647303860872, -18.47759065022490432 ) ) ;
#8689=FACE_OUTER_BOUND ( 'NONE', #9016, .T. ) ;
#8691=ORIENTED_EDGE ( 'NONE', *, *, #2008, .T. ) ;
#8713=DIRECTION ( 'NONE',  ( -1.000000000000000000, -0.000000000000000000, -0.000000000000000000 ) ) ;
#8727=DIRECTION ( 'NONE',  ( 1.000000000000000000, 0.000000000000000000, 0.000000000000000000 ) ) ;
#8730=DIRECTION ( 'NONE',  ( 0.000000000000000000, 0.000000000000000000, -1.000000000000000000 ) ) ;
#8732=DIRECTION ( 'NONE',  ( 0.000000000000000000, 0.000000000000000000, 1.000000000000000000 ) ) ;
#8742=ORIENTED_EDGE ( 'NONE', *, *, #6250, .T. ) ;
#8757=EDGE_CURVE ( 'NONE', #6239, #4910, #3509, .T. ) ;
#8759=FACE_OUTER_BOUND ( 'NONE', #1845, .T. ) ;
#8761=FACE_OUTER_BOUND ( 'NONE', #242, .T. ) ;
#8782=CARTESIAN_POINT ( 'NONE',  ( 4.000000000000000000, -18.47759065022712832, 6.903668647304566974 ) ) ;
#8785=CIRCLE ( 'NONE', #4653, 0.7500000000017874591 ) ;
#8791=CYLINDRICAL_SURFACE ( 'NONE', #4276, 1.560000000001466436 ) ;
#8802=CARTESIAN_POINT ( 'NONE',  ( 0.000000000000000000, 0.000000000000000000, 0.000000000000000000 ) ) ;
#8830=AXIS2_PLACEMENT_3D ( 'NONE', #8214, #8977, #8494 ) ;
#8834=ORIENTED_EDGE ( 'NONE', *, *, #5117, .T. ) ;
#8837=CIRCLE ( 'NONE', #100, 1.560000000002236709 ) ;
#8838=LINE ( 'NONE', #4376, #2896 ) ;
#8839=DIRECTION ( 'NONE',  ( -1.000000000000000000, -0.000000000000000000, -0.000000000000000000 ) ) ;
#8844=CARTESIAN_POINT ( 'NONE',  ( 0.000000000000000000, -14.14213562373248401, -12.58213562372718641 ) ) ;
#8849=VECTOR ( 'NONE', #2837, 1000.000000000000114 ) ;
#8852=EDGE_CURVE ( 'NONE', #4140, #4695, #6542, .T. ) ;
#8863=DIRECTION ( 'NONE',  ( 0.000000000000000000, 0.000000000000000000, 1.000000000000000000 ) ) ;
#8877=CARTESIAN_POINT ( 'NONE',  ( 0.000000000000000000, -18.47759065022712832, 7.653668647304757044 ) ) ;
#8883=ORIENTED_EDGE ( 'NONE', *, *, #5348, .T. ) ;
#8892=AXIS2_PLACEMENT_3D ( 'NONE', #5778, #7029, #1206 ) ;
#8896=DIRECTION ( 'NONE',  ( 0.000000000000000000, 0.000000000000000000, 1.000000000000000000 ) ) ;
#8904=EDGE_LOOP ( 'NONE', ( #5403, #6147, #1117, #4770 ) ) ;
#8913=CARTESIAN_POINT ( 'NONE',  ( 5.000000000000000000, -18.47759065022712832, 7.653668647304757044 ) ) ;
#8914=DIRECTION ( 'NONE',  ( -1.000000000000000000, -0.000000000000000000, -0.000000000000000000 ) ) ;
#8915=ORIENTED_EDGE ( 'NONE', *, *, #22, .T. ) ;
#8927=ORIENTED_EDGE ( 'NONE', *, *, #5865, .F. ) ;
#8944=VERTEX_POINT ( 'NONE', #3659 ) ;
#8950=CARTESIAN_POINT ( 'NONE',  ( 4.000000000000000000, 7.653668647302530381, 18.47759065022802716 ) ) ;
#8970=ORIENTED_EDGE ( 'NONE', *, *, #3140, .F. ) ;
#8977=DIRECTION ( 'NONE',  ( -1.000000000000000000, 0.000000000000000000, 0.000000000000000000 ) ) ;
#8979=DIRECTION ( 'NONE',  ( -1.000000000000000000, 0.000000000000000000, 0.000000000000000000 ) ) ;
#8986=EDGE_CURVE ( 'NONE', #2437, #7251, #5436, .T. ) ;
#8990=CYLINDRICAL_SURFACE ( 'NONE', #9150, 1.560000000000134168 ) ;
#8996=EDGE_LOOP ( 'NONE', ( #732, #2872, #4226, #2521 ) ) ;
#8998=VERTEX_POINT ( 'NONE', #5290 ) ;
#9002=AXIS2_PLACEMENT_3D ( 'NONE', #682, #6604, #7987 ) ;
#9004=CIRCLE ( 'NONE', #7157, 0.7500000000013684609 ) ;
#9005=DIRECTION ( 'NONE',  ( -1.000000000000000000, 0.000000000000000000, 0.000000000000000000 ) ) ;
#9010=CIRCLE ( 'NONE', #1652, 22.50000000000000000 ) ;
#9016=EDGE_LOOP ( 'NONE', ( #4190, #1670, #1996, #4961 ) ) ;
#9024=ORIENTED_EDGE ( 'NONE', *, *, #9403, .F. ) ;
#9025=ORIENTED_EDGE ( 'NONE', *, *, #154, .T. ) ;
#9028=AXIS2_PLACEMENT_3D ( 'NONE', #2636, #4204, #3529 ) ;
#9030=CIRCLE ( 'NONE', #2754, 0.7499999999982936982 ) ;
#9032=CARTESIAN_POINT ( 'NONE',  ( 0.000000000000000000, 2.694222958124177598E-15, 22.00000000000000711 ) ) ;
#9034=CYLINDRICAL_SURFACE ( 'NONE', #1963, 0.7500000000017874591 ) ;
#9036=VECTOR ( 'NONE', #3800, 1000.000000000000000 ) ;
#9037=VERTEX_POINT ( 'NONE', #246 ) ;
#9041=DIRECTION ( 'NONE',  ( 0.000000000000000000, 0.000000000000000000, 1.000000000000000000 ) ) ;
#9048=PRODUCT_DEFINITION ( 'UNKNOWN', '', #2695, #7495 ) ;
#9059=ORIENTED_EDGE ( 'NONE', *, *, #4943, .F. ) ;
#9063=ORIENTED_EDGE ( 'NONE', *, *, #6043, .T. ) ;
#9066=EDGE_LOOP ( 'NONE', ( #1054, #7662, #9063, #3789 ) ) ;
#9075=AXIS2_PLACEMENT_3D ( 'NONE', #2379, #5307, #3673 ) ;
#9077=DIRECTION ( 'NONE',  ( -1.000000000000000000, 0.000000000000000000, 0.000000000000000000 ) ) ;
#9079=CARTESIAN_POINT ( 'NONE',  ( 5.000000000000000000, -14.14213562373112154, 15.70213562373564820 ) ) ;
#9114=ORIENTED_EDGE ( 'NONE', *, *, #8243, .T. ) ;
#9115=VECTOR ( 'NONE', #1310, 1000.000000000000000 ) ;
#9123=DIRECTION ( 'NONE',  ( 0.000000000000000000, 0.000000000000000000, 1.000000000000000000 ) ) ;
#9124=EDGE_CURVE ( 'NONE', #6180, #5267, #2114, .T. ) ;
#9139=EDGE_CURVE ( 'NONE', #3367, #9386, #7483, .T. ) ;
#9150=AXIS2_PLACEMENT_3D ( 'NONE', #8227, #3958, #925 ) ;
#9154=AXIS2_PLACEMENT_3D ( 'NONE', #680, #3611, #6549 ) ;
#9156=AXIS2_PLACEMENT_3D ( 'NONE', #8123, #5858, #1529 ) ;
#9164=AXIS2_PLACEMENT_3D ( 'NONE', #4402, #3733, #1150 ) ;
#9166=ADVANCED_FACE ( 'NONE', ( #6257 ), #8408, .T. ) ;
#9168=DIRECTION ( 'NONE',  ( 0.000000000000000000, 0.000000000000000000, 1.000000000000000000 ) ) ;
#9176=CIRCLE ( 'NONE', #5191, 1.560000000000000719 ) ;
#9177=CIRCLE ( 'NONE', #1825, 1.560000000001265263 ) ;
#9187=ORIENTED_EDGE ( 'NONE', *, *, #5666, .F. ) ;
#9193=CARTESIAN_POINT ( 'NONE',  ( 5.000000000000000000, -9.628187502531647418E-13, -18.43999999999823913 ) ) ;
#9194=ORIENTED_EDGE ( 'NONE', *, *, #5242, .T. ) ;
#9197=EDGE_LOOP ( 'NONE', ( #1129, #4148 ) ) ;
#9202=DIRECTION ( 'NONE',  ( 1.000000000000000000, 0.000000000000000000, 0.000000000000000000 ) ) ;
#9230=ORIENTED_EDGE ( 'NONE', *, *, #7060, .T. ) ;
#9232=FACE_BOUND ( 'NONE', #7035, .T. ) ;
#9245=LINE ( 'NONE', #6334, #5909 ) ;
#9246=DIRECTION ( 'NONE',  ( 0.000000000000000000, 0.000000000000000000, -1.000000000000000000 ) ) ;
#9270=ADVANCED_FACE ( 'NONE', ( #2536, #5516 ), #282, .T. ) ;
#9271=DIRECTION ( 'NONE',  ( 1.000000000000000000, 0.000000000000000000, 0.000000000000000000 ) ) ;
#9272=ORIENTED_EDGE ( 'NONE', *, *, #7943, .F. ) ;
#9273=ORIENTED_EDGE ( 'NONE', *, *, #6358, .F. ) ;
#9285=EDGE_LOOP ( 'NONE', ( #601, #3195 ) ) ;
#9296=CIRCLE ( 'NONE', #4706, 1.560000000000002274 ) ;
#9298=ORIENTED_EDGE ( 'NONE', *, *, #7837, .F. ) ;
#9301=AXIS2_PLACEMENT_3D ( 'NONE', #4624, #4215, #4317 ) ;
#9307=DIRECTION ( 'NONE',  ( -1.000000000000000000, -0.000000000000000000, -0.000000000000000000 ) ) ;
#9308=CIRCLE ( 'NONE', #4727, 17.50000000000000000 ) ;
#9315=ORIENTED_EDGE ( 'NONE', *, *, #2004, .F. ) ;
#9316=EDGE_CURVE ( 'NONE', #2688, #6912, #322, .T. ) ;
#9318=CIRCLE ( 'NONE', #5954, 0.7499999999986606269 ) ;
#9321=FACE_OUTER_BOUND ( 'NONE', #5037, .T. ) ;
#9323=DIRECTION ( 'NONE',  ( 0.000000000000000000, 0.000000000000000000, 1.000000000000000000 ) ) ;
#9328=EDGE_LOOP ( 'NONE', ( #3980, #4283 ) ) ;
#9332=CIRCLE ( 'NONE', #1977, 1.560000000001265263 ) ;
#9333=CARTESIAN_POINT ( 'NONE',  ( 5.000000000000000000, 14.14213562373247868, 15.70213562373191962 ) ) ;
#9337=CARTESIAN_POINT ( 'NONE',  ( 0.000000000000000000, -14.14213562373112154, 12.58213562373271621 ) ) ;
#9338=EDGE_LOOP ( 'NONE', ( #2064, #9194, #3614, #7647 ) ) ;
#9340=VERTEX_POINT ( 'NONE', #7180 ) ;
#9355=DIRECTION ( 'NONE',  ( -1.000000000000000000, -0.000000000000000000, -0.000000000000000000 ) ) ;
#9361=EDGE_CURVE ( 'NONE', #943, #7855, #1265, .T. ) ;
#9362=CARTESIAN_POINT ( 'NONE',  ( 5.000000000000000000, 7.653668647302530381, 19.22759065022631830 ) ) ;
#9366=VERTEX_POINT ( 'NONE', #6473 ) ;
#9368=VERTEX_POINT ( 'NONE', #6291 ) ;
#9371=CARTESIAN_POINT ( 'NONE',  ( 0.000000000000000000, 20.00000000000120437, 7.412591687719288072E-13 ) ) ;
#9374=FACE_BOUND ( 'NONE', #1202, .T. ) ;
#9379=FACE_BOUND ( 'NONE', #6577, .T. ) ;
#9386=VERTEX_POINT ( 'NONE', #5612 ) ;
#9397=DIRECTION ( 'NONE',  ( 0.000000000000000000, 0.000000000000000000, -1.000000000000000000 ) ) ;
#9403=EDGE_CURVE ( 'NONE', #2622, #7382, #4841, .T. ) ;
#9411=EDGE_LOOP ( 'NONE', ( #7625, #3391, #1173, #281 ) ) ;
#9421=AXIS2_PLACEMENT_3D ( 'NONE', #6523, #5848, #2960 ) ;
#9428=CYLINDRICAL_SURFACE ( 'NONE', #5788, 0.7499999999986606269 ) ;
#9433=AXIS2_PLACEMENT_3D ( 'NONE', #7574, #8339, #1762 ) ;
#9434=ORIENTED_EDGE ( 'NONE', *, *, #7924, .F. ) ;
#9439=DIRECTION ( 'NONE',  ( -1.000000000000000000, 0.000000000000000000, 0.000000000000000000 ) ) ;
#9454=EDGE_LOOP ( 'NONE', ( #6800, #6761 ) ) ;
#9461=AXIS2_PLACEMENT_3D ( 'NONE', #5013, #2672, #2855 ) ;
#9509=COLOUR_RGB('Light Blue',0.38,0.62,0.78);
#9510=FILL_AREA_STYLE_COLOUR('',#9509);
#9511=FILL_AREA_STYLE('',(#9510));
#9512=SURFACE_STYLE_FILL_AREA(#9511);
#9513=SURFACE_SIDE_STYLE('',(#9512));
#9514=SURFACE_STYLE_USAGE(.BOTH.,#9513);
#9515=PRESENTATION_STYLE_ASSIGNMENT((#9514));
ENDSEC;
END-ISO-10303-21;
